ISO-10303-21;
HEADER;
/* Generated by software containing ST-Developer
 * from STEP Tools, Inc. (www.steptools.com) 
 */

FILE_DESCRIPTION(
/* description */ (''),
/* implementation_level */ '2;1');

FILE_NAME(
/* name */ 'Bearing_01.step',
/* time_stamp */ '2026-10-05T21:54:13-07:00',
/* author */ (''),
/* organization */ (''),
/* preprocessor_version */ 'ST-DEVELOPER v20.2',
/* originating_system */ 'Autodesk Translation Framework v15.15.0.0',
/* authorisation */ '');

FILE_SCHEMA (('AUTOMOTIVE_DESIGN { 1 0 10303 214 3 1 1 }'));
ENDSEC;

DATA;
#10=MECHANICAL_DESIGN_GEOMETRIC_PRESENTATION_REPRESENTATION('',(#193,#194,#195,#196,#197,#198,#199,#200,#201,#202),#43781);
#43=SPHERICAL_SURFACE('',#13654,3.56616156686793);
#44=SPHERICAL_SURFACE('',#13656,3.56616156686793);
#45=SPHERICAL_SURFACE('',#13658,3.56616156686793);
#46=SPHERICAL_SURFACE('',#13660,3.56616156686793);
#47=SPHERICAL_SURFACE('',#13662,3.56616156686793);
#48=SPHERICAL_SURFACE('',#13664,3.56616156686793);
#49=SPHERICAL_SURFACE('',#13666,3.56616156686793);
#50=SPHERICAL_SURFACE('',#13720,3.56616156686792);
#51=SPHERICAL_SURFACE('',#13734,3.56616156686792);
#52=SPHERICAL_SURFACE('',#13748,3.56616156686792);
#53=SPHERICAL_SURFACE('',#13762,3.56616156686792);
#54=SPHERICAL_SURFACE('',#13776,3.56616156686792);
#55=SPHERICAL_SURFACE('',#13790,3.56616156686792);
#56=SPHERICAL_SURFACE('',#13800,3.56616156686792);
#99=CONICAL_SURFACE('',#13643,8.14999999999999,0.785398163397436);
#100=CONICAL_SURFACE('',#13646,7.5,0.785398163397437);
#101=CONICAL_SURFACE('',#13702,20.35,0.785398163397442);
#102=CONICAL_SURFACE('',#13705,21.,0.785398163397442);
#115=TOROIDAL_SURFACE('',#13628,14.25,3.56616156686793);
#116=TOROIDAL_SURFACE('',#13632,7.9875,0.4875);
#117=TOROIDAL_SURFACE('',#13638,7.9875,0.4875);
#118=TOROIDAL_SURFACE('',#13668,16.3271153846154,0.0585);
#119=TOROIDAL_SURFACE('',#13673,16.0931153846154,0.0585);
#120=TOROIDAL_SURFACE('',#13677,16.3271153846154,0.0585);
#121=TOROIDAL_SURFACE('',#13681,16.0931153846154,0.0585);
#122=TOROIDAL_SURFACE('',#13693,14.25,3.56616156686793);
#123=TOROIDAL_SURFACE('',#13716,2.5198520116158,1.69469015025);
#124=TOROIDAL_SURFACE('',#13730,2.5198520116158,1.69469015025);
#125=TOROIDAL_SURFACE('',#13744,2.5198520116158,1.69469015025);
#126=TOROIDAL_SURFACE('',#13758,2.5198520116158,1.69469015025);
#127=TOROIDAL_SURFACE('',#13772,2.5198520116158,1.69469015025);
#128=TOROIDAL_SURFACE('',#13786,2.5198520116158,1.69469015025);
#129=TOROIDAL_SURFACE('',#13810,2.5198520116158,1.69469015025);
#177=SHAPE_REPRESENTATION_RELATIONSHIP('SRR','None',#43815,#185);
#185=ADVANCED_BREP_SHAPE_REPRESENTATION('',(#237,#238,#239,#240,#241,#242,
#243,#244,#245,#246),#43775);
#193=STYLED_ITEM('',(#43863),#237);
#194=STYLED_ITEM('',(#43863),#238);
#195=STYLED_ITEM('',(#43863),#239);
#196=STYLED_ITEM('',(#43863),#240);
#197=STYLED_ITEM('',(#43863),#241);
#198=STYLED_ITEM('',(#43863),#242);
#199=STYLED_ITEM('',(#43863),#243);
#200=STYLED_ITEM('',(#43863),#244);
#201=STYLED_ITEM('',(#43863),#245);
#202=STYLED_ITEM('',(#43863),#246);
#237=MANIFOLD_SOLID_BREP('Body1',#13053);
#238=MANIFOLD_SOLID_BREP('Body2',#13054);
#239=MANIFOLD_SOLID_BREP('Body3',#13055);
#240=MANIFOLD_SOLID_BREP('Body4',#13056);
#241=MANIFOLD_SOLID_BREP('Body5',#13057);
#242=MANIFOLD_SOLID_BREP('Body6',#13058);
#243=MANIFOLD_SOLID_BREP('Body7',#13059);
#244=MANIFOLD_SOLID_BREP('Body8',#13060);
#245=MANIFOLD_SOLID_BREP('Body9',#13061);
#246=MANIFOLD_SOLID_BREP('Body10',#13062);
#283=FACE_BOUND('',#2304,.T.);
#284=FACE_BOUND('',#2306,.T.);
#285=FACE_BOUND('',#2329,.T.);
#286=FACE_BOUND('',#2331,.T.);
#287=FACE_BOUND('',#2333,.T.);
#288=FACE_BOUND('',#2335,.T.);
#289=FACE_BOUND('',#2337,.T.);
#290=FACE_BOUND('',#2339,.T.);
#291=FACE_BOUND('',#2341,.T.);
#292=FACE_BOUND('',#2342,.T.);
#293=FACE_BOUND('',#2344,.T.);
#294=FACE_BOUND('',#2345,.T.);
#295=FACE_BOUND('',#2347,.T.);
#296=FACE_BOUND('',#2348,.T.);
#297=FACE_BOUND('',#2350,.T.);
#298=FACE_BOUND('',#2351,.T.);
#299=FACE_BOUND('',#2353,.T.);
#300=FACE_BOUND('',#2354,.T.);
#301=FACE_BOUND('',#2356,.T.);
#302=FACE_BOUND('',#2357,.T.);
#303=FACE_BOUND('',#2359,.T.);
#304=FACE_BOUND('',#2360,.T.);
#305=FACE_BOUND('',#2362,.T.);
#306=FACE_BOUND('',#2363,.T.);
#307=FACE_BOUND('',#2365,.T.);
#308=FACE_BOUND('',#2366,.T.);
#309=FACE_BOUND('',#2368,.T.);
#310=FACE_BOUND('',#2369,.T.);
#311=FACE_BOUND('',#2371,.T.);
#312=FACE_BOUND('',#2372,.T.);
#313=FACE_BOUND('',#2374,.T.);
#314=FACE_BOUND('',#2375,.T.);
#315=FACE_BOUND('',#2377,.T.);
#316=FACE_BOUND('',#2378,.T.);
#317=FACE_BOUND('',#2380,.T.);
#318=FACE_BOUND('',#2381,.T.);
#319=FACE_BOUND('',#2387,.T.);
#320=FACE_BOUND('',#2389,.T.);
#321=FACE_BOUND('',#2395,.T.);
#322=FACE_BOUND('',#2397,.T.);
#323=FACE_BOUND('',#2407,.T.);
#324=FACE_BOUND('',#2409,.T.);
#325=FACE_BOUND('',#2419,.T.);
#326=FACE_BOUND('',#2421,.T.);
#327=FACE_BOUND('',#2431,.T.);
#328=FACE_BOUND('',#2433,.T.);
#329=FACE_BOUND('',#2443,.T.);
#330=FACE_BOUND('',#2445,.T.);
#331=FACE_BOUND('',#2455,.T.);
#332=FACE_BOUND('',#2457,.T.);
#611=B_SPLINE_CURVE_WITH_KNOTS('',3,(#38185,#38186,#38187,#38188,#38189,
#38190),.UNSPECIFIED.,.F.,.F.,(4,2,4),(0.436494357616827,0.49057908163088,
0.523269669927392),.UNSPECIFIED.);
#612=B_SPLINE_CURVE_WITH_KNOTS('',3,(#38192,#38193,#38194,#38195,#38196,
#38197,#38198,#38199,#38200,#38201,#38202,#38203,#38204,#38205,#38206,#38207,
#38208,#38209,#38210),.UNSPECIFIED.,.F.,.F.,(4,3,3,3,3,3,4),(1.21344063784114,
1.25510987200879,1.29073244309217,1.33189452838103,1.37317594357341,1.41463545273866,
1.43283480298246),.UNSPECIFIED.);
#613=B_SPLINE_CURVE_WITH_KNOTS('',3,(#38212,#38213,#38214,#38215,#38216,
#38217),.UNSPECIFIED.,.F.,.F.,(4,2,4),(0.436494357616828,0.49057908163088,
0.523269669927516),.UNSPECIFIED.);
#614=B_SPLINE_CURVE_WITH_KNOTS('',3,(#38218,#38219,#38220,#38221,#38222,
#38223,#38224,#38225,#38226,#38227,#38228,#38229,#38230,#38231,#38232,#38233,
#38234,#38235,#38236),.UNSPECIFIED.,.F.,.F.,(4,3,3,3,3,3,4),(-1.40481265039417,
-1.36522996541144,-1.32585540726346,-1.28679683363995,-1.26015734748852,
-1.21999608757349,-1.1843388203003),.UNSPECIFIED.);
#615=B_SPLINE_CURVE_WITH_KNOTS('',3,(#38239,#38240,#38241,#38242,#38243,
#38244),.UNSPECIFIED.,.F.,.F.,(4,2,4),(1.43904665659616,1.47173724489264,
1.52582196890669),.UNSPECIFIED.);
#616=B_SPLINE_CURVE_WITH_KNOTS('',3,(#38246,#38247,#38248,#38249,#38250,
#38251,#38252,#38253,#38254,#38255,#38256,#38257,#38258,#38259,#38260,#38261,
#38262,#38263,#38264),.UNSPECIFIED.,.F.,.F.,(4,3,3,3,3,3,4),(-0.110253525235352,
-0.070240741437667,-0.0308586443223014,0.,0.0392000421916667,0.0788707706427855,
0.110060546834446),.UNSPECIFIED.);
#617=B_SPLINE_CURVE_WITH_KNOTS('',3,(#38266,#38267,#38268,#38269,#38270,
#38271),.UNSPECIFIED.,.F.,.F.,(4,2,4),(1.43904665659616,1.47173724489264,
1.52582196890582),.UNSPECIFIED.);
#618=B_SPLINE_CURVE_WITH_KNOTS('',3,(#38272,#38273,#38274,#38275,#38276,
#38277,#38278,#38279,#38280,#38281,#38282,#38283,#38284,#38285,#38286,#38287,
#38288,#38289,#38290),.UNSPECIFIED.,.F.,.F.,(4,3,3,3,3,3,4),(2.53632937909178,
2.57775416224765,2.61898206719527,2.6459019021663,2.68717408326041,2.72876559667488,
2.75562831582286),.UNSPECIFIED.);
#619=B_SPLINE_CURVE_WITH_KNOTS('',3,(#38300,#38301,#38302,#38303,#38304,
#38305,#38306),.UNSPECIFIED.,.F.,.F.,(4,3,4),(1.98904556960248,2.09488046175532,
2.20071535390815),.UNSPECIFIED.);
#620=B_SPLINE_CURVE_WITH_KNOTS('',3,(#38310,#38311,#38312,#38313,#38314,
#38315,#38316),.UNSPECIFIED.,.F.,.F.,(4,3,4),(-0.105611957753097,0.,0.105611957753097),
 .UNSPECIFIED.);
#621=B_SPLINE_CURVE_WITH_KNOTS('',3,(#38321,#38322,#38323,#38324,#38325,
#38326),.UNSPECIFIED.,.F.,.F.,(4,2,4),(-1.17106027221854,-1.06544831446544,
-0.959836356712345),.UNSPECIFIED.);
#622=B_SPLINE_CURVE_WITH_KNOTS('',3,(#38329,#38330,#38331,#38332,#38333,
#38334),.UNSPECIFIED.,.F.,.F.,(4,2,4),(0.941605338724826,1.04744023087766,
1.15327512303049),.UNSPECIFIED.);
#623=B_SPLINE_CURVE_WITH_KNOTS('',3,(#38347,#38348,#38349,#38350,#38351,
#38352),.UNSPECIFIED.,.F.,.F.,(4,2,4),(0.436494357616816,0.49057908163088,
0.523269669927352),.UNSPECIFIED.);
#624=B_SPLINE_CURVE_WITH_KNOTS('',3,(#38354,#38355,#38356,#38357,#38358,
#38359,#38360,#38361,#38362,#38363,#38364,#38365,#38366,#38367,#38368,#38369,
#38370,#38371,#38372),.UNSPECIFIED.,.F.,.F.,(4,3,3,3,3,3,4),(1.21344063784117,
1.2551098720088,1.29073244309219,1.33189452838105,1.37317594357344,1.41463545273871,
1.43283480298249),.UNSPECIFIED.);
#625=B_SPLINE_CURVE_WITH_KNOTS('',3,(#38374,#38375,#38376,#38377,#38378,
#38379),.UNSPECIFIED.,.F.,.F.,(4,2,4),(0.436484426249651,0.490578640084517,
0.523250481795878),.UNSPECIFIED.);
#626=B_SPLINE_CURVE_WITH_KNOTS('',3,(#38380,#38381,#38382,#38383,#38384,
#38385,#38386,#38387,#38388,#38389,#38390,#38391,#38392,#38393,#38394,#38395,
#38396,#38397,#38398),.UNSPECIFIED.,.F.,.F.,(4,3,3,3,3,3,4),(-1.40481265039413,
-1.36522996541145,-1.32585540726349,-1.28679683363998,-1.2601573474885,
-1.21999608757352,-1.18433882030031),.UNSPECIFIED.);
#627=B_SPLINE_CURVE_WITH_KNOTS('',3,(#38401,#38402,#38403,#38404,#38405,
#38406),.UNSPECIFIED.,.F.,.F.,(4,2,4),(1.43906407854219,1.47173592025355,
1.52583013408841),.UNSPECIFIED.);
#628=B_SPLINE_CURVE_WITH_KNOTS('',3,(#38408,#38409,#38410,#38411,#38412,
#38413,#38414,#38415,#38416,#38417,#38418,#38419,#38420,#38421,#38422,#38423,
#38424,#38425,#38426),.UNSPECIFIED.,.F.,.F.,(4,3,3,3,3,3,4),(-0.110253525235351,
-0.0702407414376934,-0.0308586443223274,0.,0.0392000421916682,0.0788707706427895,
0.110060546834446),.UNSPECIFIED.);
#629=B_SPLINE_CURVE_WITH_KNOTS('',3,(#38428,#38429,#38430,#38431,#38432,
#38433),.UNSPECIFIED.,.F.,.F.,(4,2,4),(1.43906407854219,1.47173592025355,
1.52583013408754),.UNSPECIFIED.);
#630=B_SPLINE_CURVE_WITH_KNOTS('',3,(#38434,#38435,#38436,#38437,#38438,
#38439,#38440,#38441,#38442,#38443,#38444,#38445,#38446,#38447,#38448,#38449,
#38450,#38451,#38452),.UNSPECIFIED.,.F.,.F.,(4,3,3,3,3,3,4),(2.53632937909181,
2.57775416224765,2.61898206719527,2.64590190216633,2.68717408326044,2.72876559667489,
2.75562831582288),.UNSPECIFIED.);
#631=B_SPLINE_CURVE_WITH_KNOTS('',3,(#38462,#38463,#38464,#38465,#38466,
#38467,#38468),.UNSPECIFIED.,.F.,.F.,(4,3,4),(1.98904556960249,2.09488046175532,
2.20071535390816),.UNSPECIFIED.);
#632=B_SPLINE_CURVE_WITH_KNOTS('',3,(#38472,#38473,#38474,#38475,#38476,
#38477,#38478),.UNSPECIFIED.,.F.,.F.,(4,3,4),(-0.105611957753097,0.,0.105611957753097),
 .UNSPECIFIED.);
#633=B_SPLINE_CURVE_WITH_KNOTS('',3,(#38483,#38484,#38485,#38486,#38487,
#38488),.UNSPECIFIED.,.F.,.F.,(4,2,4),(-1.17106027221854,-1.06544831446544,
-0.959836356712344),.UNSPECIFIED.);
#634=B_SPLINE_CURVE_WITH_KNOTS('',3,(#38491,#38492,#38493,#38494,#38495,
#38496),.UNSPECIFIED.,.F.,.F.,(4,2,4),(0.941605338724829,1.04744023087766,
1.15327512303049),.UNSPECIFIED.);
#635=B_SPLINE_CURVE_WITH_KNOTS('',3,(#38509,#38510,#38511,#38512,#38513,
#38514),.UNSPECIFIED.,.F.,.F.,(4,2,4),(0.436484426249655,0.490578640084517,
0.523250481795882),.UNSPECIFIED.);
#636=B_SPLINE_CURVE_WITH_KNOTS('',3,(#38516,#38517,#38518,#38519,#38520,
#38521,#38522,#38523,#38524,#38525,#38526,#38527,#38528,#38529,#38530,#38531,
#38532,#38533,#38534),.UNSPECIFIED.,.F.,.F.,(4,3,3,3,3,3,4),(2.53632937909178,
2.57775416224762,2.61898206719525,2.64590190216632,2.68717408326042,2.72876559667488,
2.75562831582289),.UNSPECIFIED.);
#637=B_SPLINE_CURVE_WITH_KNOTS('',3,(#38536,#38537,#38538,#38539,#38540,
#38541),.UNSPECIFIED.,.F.,.F.,(4,2,4),(0.436494357616821,0.49057908163088,
0.523269669927365),.UNSPECIFIED.);
#638=B_SPLINE_CURVE_WITH_KNOTS('',3,(#38542,#38543,#38544,#38545,#38546,
#38547,#38548,#38549,#38550,#38551,#38552,#38553,#38554,#38555,#38556,#38557,
#38558,#38559,#38560),.UNSPECIFIED.,.F.,.F.,(4,3,3,3,3,3,4),(-0.110253525235353,
-0.0702407414376493,-0.0308586443222864,0.,0.0392000421916586,0.0788707706427754,
0.110060546834447),.UNSPECIFIED.);
#639=B_SPLINE_CURVE_WITH_KNOTS('',3,(#38563,#38564,#38565,#38566,#38567,
#38568),.UNSPECIFIED.,.F.,.F.,(4,2,4),(1.43906407854219,1.47173592025355,
1.52583013408841),.UNSPECIFIED.);
#640=B_SPLINE_CURVE_WITH_KNOTS('',3,(#38570,#38571,#38572,#38573,#38574,
#38575,#38576,#38577,#38578,#38579,#38580,#38581,#38582,#38583,#38584,#38585,
#38586,#38587,#38588),.UNSPECIFIED.,.F.,.F.,(4,3,3,3,3,3,4),(-1.40481265039415,
-1.36522996541142,-1.32585540726345,-1.28679683363994,-1.26015734748852,
-1.21999608757345,-1.18433882030032),.UNSPECIFIED.);
#641=B_SPLINE_CURVE_WITH_KNOTS('',3,(#38590,#38591,#38592,#38593,#38594,
#38595),.UNSPECIFIED.,.F.,.F.,(4,2,4),(1.43906407854219,1.47173592025355,
1.52583013408753),.UNSPECIFIED.);
#642=B_SPLINE_CURVE_WITH_KNOTS('',3,(#38596,#38597,#38598,#38599,#38600,
#38601,#38602,#38603,#38604,#38605,#38606,#38607,#38608,#38609,#38610,#38611,
#38612,#38613,#38614),.UNSPECIFIED.,.F.,.F.,(4,3,3,3,3,3,4),(1.21344063784118,
1.25510987200885,1.29073244309219,1.33189452838105,1.37317594357345,1.41463545273868,
1.43283480298247),.UNSPECIFIED.);
#643=B_SPLINE_CURVE_WITH_KNOTS('',3,(#38624,#38625,#38626,#38627,#38628,
#38629,#38630),.UNSPECIFIED.,.F.,.F.,(4,3,4),(1.98904556960249,2.09488046175532,
2.20071535390815),.UNSPECIFIED.);
#644=B_SPLINE_CURVE_WITH_KNOTS('',3,(#38634,#38635,#38636,#38637,#38638,
#38639,#38640),.UNSPECIFIED.,.F.,.F.,(4,3,4),(-0.105611957753096,0.,0.105611957753097),
 .UNSPECIFIED.);
#645=B_SPLINE_CURVE_WITH_KNOTS('',3,(#38645,#38646,#38647,#38648,#38649,
#38650),.UNSPECIFIED.,.F.,.F.,(4,2,4),(-1.17106027221854,-1.06544831446544,
-0.959836356712344),.UNSPECIFIED.);
#646=B_SPLINE_CURVE_WITH_KNOTS('',3,(#38653,#38654,#38655,#38656,#38657,
#38658),.UNSPECIFIED.,.F.,.F.,(4,2,4),(0.941605338724827,1.04744023087766,
1.15327512303049),.UNSPECIFIED.);
#647=B_SPLINE_CURVE_WITH_KNOTS('',3,(#38671,#38672,#38673,#38674,#38675,
#38676),.UNSPECIFIED.,.F.,.F.,(4,2,4),(0.436494357616822,0.49057908163088,
0.523269669927398),.UNSPECIFIED.);
#648=B_SPLINE_CURVE_WITH_KNOTS('',3,(#38678,#38679,#38680,#38681,#38682,
#38683,#38684,#38685,#38686,#38687,#38688,#38689,#38690,#38691,#38692,#38693,
#38694,#38695,#38696),.UNSPECIFIED.,.F.,.F.,(4,3,3,3,3,3,4),(2.53632937909185,
2.57775416224773,2.61898206719535,2.64590190216638,2.6871740832605,2.72876559667492,
2.75562831582295),.UNSPECIFIED.);
#649=B_SPLINE_CURVE_WITH_KNOTS('',3,(#38698,#38699,#38700,#38701,#38702,
#38703),.UNSPECIFIED.,.F.,.F.,(4,2,4),(0.436484426249657,0.490578640084517,
0.523250481796065),.UNSPECIFIED.);
#650=B_SPLINE_CURVE_WITH_KNOTS('',3,(#38704,#38705,#38706,#38707,#38708,
#38709,#38710,#38711,#38712,#38713,#38714,#38715,#38716,#38717,#38718,#38719,
#38720,#38721,#38722),.UNSPECIFIED.,.F.,.F.,(4,3,3,3,3,3,4),(-0.110253525235377,
-0.070240741437708,-0.0308586443223363,0.,0.03920004219167,0.0788707706428437,
0.110060546834472),.UNSPECIFIED.);
#651=B_SPLINE_CURVE_WITH_KNOTS('',3,(#38725,#38726,#38727,#38728,#38729,
#38730),.UNSPECIFIED.,.F.,.F.,(4,2,4),(1.43904665659616,1.47173724489264,
1.52582196890669),.UNSPECIFIED.);
#652=B_SPLINE_CURVE_WITH_KNOTS('',3,(#38732,#38733,#38734,#38735,#38736,
#38737,#38738,#38739,#38740,#38741,#38742,#38743,#38744,#38745,#38746,#38747,
#38748,#38749,#38750),.UNSPECIFIED.,.F.,.F.,(4,3,3,3,3,3,4),(-1.40481265039411,
-1.36522996541141,-1.32585540726345,-1.28679683363994,-1.26015734748849,
-1.21999608757351,-1.1843388203003),.UNSPECIFIED.);
#653=B_SPLINE_CURVE_WITH_KNOTS('',3,(#38752,#38753,#38754,#38755,#38756,
#38757),.UNSPECIFIED.,.F.,.F.,(4,2,4),(1.43904665659616,1.47173724489264,
1.52582196890583),.UNSPECIFIED.);
#654=B_SPLINE_CURVE_WITH_KNOTS('',3,(#38758,#38759,#38760,#38761,#38762,
#38763,#38764,#38765,#38766,#38767,#38768,#38769,#38770,#38771,#38772,#38773,
#38774,#38775,#38776),.UNSPECIFIED.,.F.,.F.,(4,3,3,3,3,3,4),(1.2134406378412,
1.25510987200883,1.29073244309221,1.33189452838107,1.37317594357346,1.41463545273868,
1.43283480298249),.UNSPECIFIED.);
#655=B_SPLINE_CURVE_WITH_KNOTS('',3,(#38786,#38787,#38788,#38789,#38790,
#38791,#38792),.UNSPECIFIED.,.F.,.F.,(4,3,4),(1.98904556960248,2.09488046175532,
2.20071535390815),.UNSPECIFIED.);
#656=B_SPLINE_CURVE_WITH_KNOTS('',3,(#38796,#38797,#38798,#38799,#38800,
#38801,#38802),.UNSPECIFIED.,.F.,.F.,(4,3,4),(-0.105611957753097,0.,0.105611957753097),
 .UNSPECIFIED.);
#657=B_SPLINE_CURVE_WITH_KNOTS('',3,(#38807,#38808,#38809,#38810,#38811,
#38812),.UNSPECIFIED.,.F.,.F.,(4,2,4),(-1.17106027221854,-1.06544831446544,
-0.959836356712344),.UNSPECIFIED.);
#658=B_SPLINE_CURVE_WITH_KNOTS('',3,(#38815,#38816,#38817,#38818,#38819,
#38820),.UNSPECIFIED.,.F.,.F.,(4,2,4),(0.941605338724826,1.04744023087766,
1.15327512303049),.UNSPECIFIED.);
#659=B_SPLINE_CURVE_WITH_KNOTS('',3,(#38833,#38834,#38835,#38836,#38837,
#38838),.UNSPECIFIED.,.F.,.F.,(4,2,4),(0.436494357616821,0.49057908163088,
0.523269669927355),.UNSPECIFIED.);
#660=B_SPLINE_CURVE_WITH_KNOTS('',3,(#38840,#38841,#38842,#38843,#38844,
#38845,#38846,#38847,#38848,#38849,#38850,#38851,#38852,#38853,#38854,#38855,
#38856,#38857,#38858),.UNSPECIFIED.,.F.,.F.,(4,3,3,3,3,3,4),(2.53632937909179,
2.57775416224772,2.61898206719534,2.64590190216632,2.68717408326042,2.72876559667486,
2.75562831582289),.UNSPECIFIED.);
#661=B_SPLINE_CURVE_WITH_KNOTS('',3,(#38860,#38861,#38862,#38863,#38864,
#38865),.UNSPECIFIED.,.F.,.F.,(4,2,4),(0.436494357616821,0.49057908163088,
0.523269669927355),.UNSPECIFIED.);
#662=B_SPLINE_CURVE_WITH_KNOTS('',3,(#38866,#38867,#38868,#38869,#38870,
#38871,#38872,#38873,#38874,#38875,#38876,#38877,#38878,#38879,#38880,#38881,
#38882,#38883,#38884),.UNSPECIFIED.,.F.,.F.,(4,3,3,3,3,3,4),(-0.110253525235352,
-0.0702407414377446,-0.0308586443223844,0.,0.039200042191676,0.0788707706427867,
0.110060546834448),.UNSPECIFIED.);
#663=B_SPLINE_CURVE_WITH_KNOTS('',3,(#38887,#38888,#38889,#38890,#38891,
#38892),.UNSPECIFIED.,.F.,.F.,(4,2,4),(1.43904665659616,1.47173724489264,
1.5258219689067),.UNSPECIFIED.);
#664=B_SPLINE_CURVE_WITH_KNOTS('',3,(#38894,#38895,#38896,#38897,#38898,
#38899,#38900,#38901,#38902,#38903,#38904,#38905,#38906,#38907,#38908,#38909,
#38910,#38911,#38912),.UNSPECIFIED.,.F.,.F.,(4,3,3,3,3,3,4),(-1.40481265039416,
-1.36522996541145,-1.32585540726348,-1.28679683363997,-1.26015734748853,
-1.21999608757355,-1.18433882030033),.UNSPECIFIED.);
#665=B_SPLINE_CURVE_WITH_KNOTS('',3,(#38914,#38915,#38916,#38917,#38918,
#38919),.UNSPECIFIED.,.F.,.F.,(4,2,4),(1.43904665659616,1.47173724489264,
1.52582196890582),.UNSPECIFIED.);
#666=B_SPLINE_CURVE_WITH_KNOTS('',3,(#38920,#38921,#38922,#38923,#38924,
#38925,#38926,#38927,#38928,#38929,#38930,#38931,#38932,#38933,#38934,#38935,
#38936,#38937,#38938),.UNSPECIFIED.,.F.,.F.,(4,3,3,3,3,3,4),(1.21344063784118,
1.25510987200879,1.29073244309219,1.33189452838105,1.37317594357344,1.41463545273868,
1.43283480298247),.UNSPECIFIED.);
#667=B_SPLINE_CURVE_WITH_KNOTS('',3,(#38948,#38949,#38950,#38951,#38952,
#38953,#38954),.UNSPECIFIED.,.F.,.F.,(4,3,4),(1.98904556960248,2.09488046175532,
2.20071535390815),.UNSPECIFIED.);
#668=B_SPLINE_CURVE_WITH_KNOTS('',3,(#38958,#38959,#38960,#38961,#38962,
#38963,#38964),.UNSPECIFIED.,.F.,.F.,(4,3,4),(-0.105611957753098,0.,0.105611957753098),
 .UNSPECIFIED.);
#669=B_SPLINE_CURVE_WITH_KNOTS('',3,(#38969,#38970,#38971,#38972,#38973,
#38974),.UNSPECIFIED.,.F.,.F.,(4,2,4),(-1.17106027221854,-1.06544831446544,
-0.959836356712345),.UNSPECIFIED.);
#670=B_SPLINE_CURVE_WITH_KNOTS('',3,(#38977,#38978,#38979,#38980,#38981,
#38982),.UNSPECIFIED.,.F.,.F.,(4,2,4),(0.941605338724826,1.04744023087766,
1.15327512303049),.UNSPECIFIED.);
#671=B_SPLINE_CURVE_WITH_KNOTS('',3,(#38995,#38996,#38997,#38998,#38999,
#39000,#39001,#39002,#39003,#39004,#39005,#39006,#39007,#39008,#39009,#39010,
#39011,#39012,#39013),.UNSPECIFIED.,.F.,.F.,(4,3,3,3,3,3,4),(2.47883976068978,
2.51859129056809,2.55786629068885,2.58890030752247,2.62818560996811,2.66809093310445,
2.69915383275782),.UNSPECIFIED.);
#672=B_SPLINE_CURVE_WITH_KNOTS('',3,(#39015,#39016,#39017,#39018,#39019,
#39020),.UNSPECIFIED.,.F.,.F.,(4,2,4),(-0.523250481795672,-0.490578640084517,
-0.436484426249653),.UNSPECIFIED.);
#673=B_SPLINE_CURVE_WITH_KNOTS('',3,(#39022,#39023,#39024,#39025,#39026,
#39027,#39028,#39029,#39030,#39031,#39032,#39033,#39034,#39035,#39036,#39037,
#39038,#39039,#39040),.UNSPECIFIED.,.F.,.F.,(4,3,3,3,3,3,4),(-0.109726413656553,
-0.0680893754924848,-0.0267736956128723,0.,0.0412006233150074,0.082597721206199,
0.109572523074534),.UNSPECIFIED.);
#674=B_SPLINE_CURVE_WITH_KNOTS('',3,(#39041,#39042,#39043,#39044,#39045,
#39046),.UNSPECIFIED.,.F.,.F.,(4,2,4),(-0.523250481795879,-0.490578640084517,
-0.43648442624966),.UNSPECIFIED.);
#675=B_SPLINE_CURVE_WITH_KNOTS('',3,(#39049,#39050,#39051,#39052,#39053,
#39054),.UNSPECIFIED.,.F.,.F.,(4,2,4),(1.43904665659616,1.47173724489264,
1.5258219689067),.UNSPECIFIED.);
#676=B_SPLINE_CURVE_WITH_KNOTS('',3,(#39056,#39057,#39058,#39059,#39060,
#39061,#39062,#39063,#39064,#39065,#39066,#39067,#39068,#39069,#39070,#39071,
#39072,#39073,#39074),.UNSPECIFIED.,.F.,.F.,(4,3,3,3,3,3,4),(-1.40481265039414,
-1.36522996541144,-1.32585540726348,-1.28679683363997,-1.26015734748851,
-1.21999608757358,-1.18433882030032),.UNSPECIFIED.);
#677=B_SPLINE_CURVE_WITH_KNOTS('',3,(#39076,#39077,#39078,#39079,#39080,
#39081),.UNSPECIFIED.,.F.,.F.,(4,2,4),(1.43904665659617,1.47173724489264,
1.52582196890583),.UNSPECIFIED.);
#678=B_SPLINE_CURVE_WITH_KNOTS('',3,(#39082,#39083,#39084,#39085,#39086,
#39087,#39088,#39089,#39090,#39091,#39092,#39093,#39094,#39095,#39096,#39097,
#39098,#39099,#39100),.UNSPECIFIED.,.F.,.F.,(4,3,3,3,3,3,4),(1.21344063784118,
1.25510987200878,1.29073244309219,1.33189452838105,1.37317594357344,1.41463545273868,
1.43283480298247),.UNSPECIFIED.);
#679=B_SPLINE_CURVE_WITH_KNOTS('',3,(#39106,#39107,#39108,#39109,#39110,
#39111),.UNSPECIFIED.,.F.,.F.,(4,2,4),(0.959836356712344,1.06544831446544,
1.17106027221854),.UNSPECIFIED.);
#680=B_SPLINE_CURVE_WITH_KNOTS('',3,(#39115,#39116,#39117,#39118,#39119,
#39120),.UNSPECIFIED.,.F.,.F.,(4,2,4),(-1.15327512303049,-1.04744023087766,
-0.941605338724826),.UNSPECIFIED.);
#681=B_SPLINE_CURVE_WITH_KNOTS('',3,(#39127,#39128,#39129,#39130,#39131,
#39132,#39133),.UNSPECIFIED.,.F.,.F.,(4,3,4),(1.98904556960249,2.09488046175532,
2.20071535390815),.UNSPECIFIED.);
#682=B_SPLINE_CURVE_WITH_KNOTS('',3,(#39137,#39138,#39139,#39140,#39141,
#39142,#39143),.UNSPECIFIED.,.F.,.F.,(4,3,4),(-0.105611957753097,0.,0.105611957753097),
 .UNSPECIFIED.);
#683=B_SPLINE_CURVE_WITH_KNOTS('',3,(#39158,#39159,#39160,#39161,#39162,
#39163,#39164),.UNSPECIFIED.,.F.,.F.,(4,3,4),(1.98904556960249,2.09488046175532,
2.20071535390815),.UNSPECIFIED.);
#684=B_SPLINE_CURVE_WITH_KNOTS('',3,(#39168,#39169,#39170,#39171,#39172,
#39173,#39174),.UNSPECIFIED.,.F.,.F.,(4,3,4),(-0.105611957753096,0.,0.105611957753097),
 .UNSPECIFIED.);
#685=B_SPLINE_CURVE_WITH_KNOTS('',3,(#39179,#39180,#39181,#39182,#39183,
#39184),.UNSPECIFIED.,.F.,.F.,(4,2,4),(-1.17106027221854,-1.06544831446544,
-0.959836356712344),.UNSPECIFIED.);
#686=B_SPLINE_CURVE_WITH_KNOTS('',3,(#39187,#39188,#39189,#39190,#39191,
#39192),.UNSPECIFIED.,.F.,.F.,(4,2,4),(0.941605338724827,1.04744023087766,
1.15327512303049),.UNSPECIFIED.);
#687=B_SPLINE_CURVE_WITH_KNOTS('',3,(#39205,#39206,#39207,#39208,#39209,
#39210),.UNSPECIFIED.,.F.,.F.,(4,2,4),(0.43648442624966,0.490578640084517,
0.523250481795913),.UNSPECIFIED.);
#688=B_SPLINE_CURVE_WITH_KNOTS('',3,(#39212,#39213,#39214,#39215,#39216,
#39217,#39218,#39219,#39220,#39221,#39222,#39223,#39224,#39225,#39226,#39227,
#39228,#39229,#39230),.UNSPECIFIED.,.F.,.F.,(4,3,3,3,3,3,4),(1.21344063784115,
1.25510987200874,1.29073244309218,1.33189452838104,1.37317594357343,1.41463545273866,
1.43283480298248),.UNSPECIFIED.);
#689=B_SPLINE_CURVE_WITH_KNOTS('',3,(#39232,#39233,#39234,#39235,#39236,
#39237),.UNSPECIFIED.,.F.,.F.,(4,2,4),(0.436494357616825,0.49057908163088,
0.523269669927497),.UNSPECIFIED.);
#690=B_SPLINE_CURVE_WITH_KNOTS('',3,(#39238,#39239,#39240,#39241,#39242,
#39243,#39244,#39245,#39246,#39247,#39248,#39249,#39250,#39251,#39252,#39253,
#39254,#39255,#39256),.UNSPECIFIED.,.F.,.F.,(4,3,3,3,3,3,4),(-1.40481265039423,
-1.36522996541152,-1.32585540726357,-1.28679683364005,-1.26015734748857,
-1.2199960875736,-1.18433882030035),.UNSPECIFIED.);
#691=B_SPLINE_CURVE_WITH_KNOTS('',3,(#39259,#39260,#39261,#39262,#39263,
#39264),.UNSPECIFIED.,.F.,.F.,(4,2,4),(1.43906407854219,1.47173592025355,
1.52583013408841),.UNSPECIFIED.);
#692=B_SPLINE_CURVE_WITH_KNOTS('',3,(#39266,#39267,#39268,#39269,#39270,
#39271,#39272,#39273,#39274,#39275,#39276,#39277,#39278,#39279,#39280,#39281,
#39282,#39283,#39284),.UNSPECIFIED.,.F.,.F.,(4,3,3,3,3,3,4),(-0.110253525235352,
-0.0702407414376601,-0.030858644322292,0.,0.0392000421916706,0.0788707706427867,
0.110060546834447),.UNSPECIFIED.);
#693=B_SPLINE_CURVE_WITH_KNOTS('',3,(#39286,#39287,#39288,#39289,#39290,
#39291),.UNSPECIFIED.,.F.,.F.,(4,2,4),(1.43906407854219,1.47173592025355,
1.52583013408754),.UNSPECIFIED.);
#694=B_SPLINE_CURVE_WITH_KNOTS('',3,(#39292,#39293,#39294,#39295,#39296,
#39297,#39298,#39299,#39300,#39301,#39302,#39303,#39304,#39305,#39306,#39307,
#39308,#39309,#39310),.UNSPECIFIED.,.F.,.F.,(4,3,3,3,3,3,4),(2.53632937909179,
2.57775416224768,2.61898206719531,2.64590190216631,2.68717408326042,2.72876559667485,
2.75562831582286),.UNSPECIFIED.);
#1075=PLANE('',#13652);
#1076=PLANE('',#13653);
#1077=PLANE('',#13710);
#1078=PLANE('',#13711);
#1079=PLANE('',#13712);
#1080=PLANE('',#13713);
#1081=PLANE('',#13714);
#1082=PLANE('',#13715);
#1083=PLANE('',#13820);
#1084=PLANE('',#13821);
#1085=PLANE('',#13822);
#1086=PLANE('',#13823);
#1087=PLANE('',#13824);
#1088=PLANE('',#13827);
#1089=PLANE('',#13832);
#1090=PLANE('',#13833);
#1091=PLANE('',#13834);
#1092=PLANE('',#13837);
#1093=PLANE('',#13848);
#1094=PLANE('',#13849);
#1095=PLANE('',#13850);
#1096=PLANE('',#13851);
#1097=PLANE('',#13852);
#1098=PLANE('',#13855);
#1099=PLANE('',#13866);
#1100=PLANE('',#13867);
#1101=PLANE('',#13868);
#1102=PLANE('',#13869);
#1103=PLANE('',#13870);
#1104=PLANE('',#13873);
#1105=PLANE('',#13884);
#1106=PLANE('',#13885);
#1107=PLANE('',#13886);
#1108=PLANE('',#13887);
#1109=PLANE('',#13888);
#1110=PLANE('',#13891);
#1111=PLANE('',#13902);
#1112=PLANE('',#13903);
#1113=PLANE('',#13904);
#1114=PLANE('',#13905);
#1115=PLANE('',#13906);
#1116=PLANE('',#13909);
#1117=PLANE('',#13920);
#1118=PLANE('',#13921);
#1119=PLANE('',#13922);
#1120=PLANE('',#13923);
#1121=PLANE('',#13924);
#1122=PLANE('',#13927);
#1123=PLANE('',#13932);
#1124=PLANE('',#13935);
#1539=FACE_OUTER_BOUND('',#2295,.T.);
#1540=FACE_OUTER_BOUND('',#2296,.T.);
#1541=FACE_OUTER_BOUND('',#2297,.T.);
#1542=FACE_OUTER_BOUND('',#2298,.T.);
#1543=FACE_OUTER_BOUND('',#2299,.T.);
#1544=FACE_OUTER_BOUND('',#2300,.T.);
#1545=FACE_OUTER_BOUND('',#2301,.T.);
#1546=FACE_OUTER_BOUND('',#2302,.T.);
#1547=FACE_OUTER_BOUND('',#2303,.T.);
#1548=FACE_OUTER_BOUND('',#2305,.T.);
#1549=FACE_OUTER_BOUND('',#2307,.T.);
#1550=FACE_OUTER_BOUND('',#2308,.T.);
#1551=FACE_OUTER_BOUND('',#2309,.T.);
#1552=FACE_OUTER_BOUND('',#2310,.T.);
#1553=FACE_OUTER_BOUND('',#2311,.T.);
#1554=FACE_OUTER_BOUND('',#2312,.T.);
#1555=FACE_OUTER_BOUND('',#2313,.T.);
#1556=FACE_OUTER_BOUND('',#2314,.T.);
#1557=FACE_OUTER_BOUND('',#2315,.T.);
#1558=FACE_OUTER_BOUND('',#2316,.T.);
#1559=FACE_OUTER_BOUND('',#2317,.T.);
#1560=FACE_OUTER_BOUND('',#2318,.T.);
#1561=FACE_OUTER_BOUND('',#2319,.T.);
#1562=FACE_OUTER_BOUND('',#2320,.T.);
#1563=FACE_OUTER_BOUND('',#2321,.T.);
#1564=FACE_OUTER_BOUND('',#2322,.T.);
#1565=FACE_OUTER_BOUND('',#2323,.T.);
#1566=FACE_OUTER_BOUND('',#2324,.T.);
#1567=FACE_OUTER_BOUND('',#2325,.T.);
#1568=FACE_OUTER_BOUND('',#2326,.T.);
#1569=FACE_OUTER_BOUND('',#2327,.T.);
#1570=FACE_OUTER_BOUND('',#2328,.T.);
#1571=FACE_OUTER_BOUND('',#2330,.T.);
#1572=FACE_OUTER_BOUND('',#2332,.T.);
#1573=FACE_OUTER_BOUND('',#2334,.T.);
#1574=FACE_OUTER_BOUND('',#2336,.T.);
#1575=FACE_OUTER_BOUND('',#2338,.T.);
#1576=FACE_OUTER_BOUND('',#2340,.T.);
#1577=FACE_OUTER_BOUND('',#2343,.T.);
#1578=FACE_OUTER_BOUND('',#2346,.T.);
#1579=FACE_OUTER_BOUND('',#2349,.T.);
#1580=FACE_OUTER_BOUND('',#2352,.T.);
#1581=FACE_OUTER_BOUND('',#2355,.T.);
#1582=FACE_OUTER_BOUND('',#2358,.T.);
#1583=FACE_OUTER_BOUND('',#2361,.T.);
#1584=FACE_OUTER_BOUND('',#2364,.T.);
#1585=FACE_OUTER_BOUND('',#2367,.T.);
#1586=FACE_OUTER_BOUND('',#2370,.T.);
#1587=FACE_OUTER_BOUND('',#2373,.T.);
#1588=FACE_OUTER_BOUND('',#2376,.T.);
#1589=FACE_OUTER_BOUND('',#2379,.T.);
#1590=FACE_OUTER_BOUND('',#2382,.T.);
#1591=FACE_OUTER_BOUND('',#2383,.T.);
#1592=FACE_OUTER_BOUND('',#2384,.T.);
#1593=FACE_OUTER_BOUND('',#2385,.T.);
#1594=FACE_OUTER_BOUND('',#2386,.T.);
#1595=FACE_OUTER_BOUND('',#2388,.T.);
#1596=FACE_OUTER_BOUND('',#2390,.T.);
#1597=FACE_OUTER_BOUND('',#2391,.T.);
#1598=FACE_OUTER_BOUND('',#2392,.T.);
#1599=FACE_OUTER_BOUND('',#2393,.T.);
#1600=FACE_OUTER_BOUND('',#2394,.T.);
#1601=FACE_OUTER_BOUND('',#2396,.T.);
#1602=FACE_OUTER_BOUND('',#2398,.T.);
#1603=FACE_OUTER_BOUND('',#2399,.T.);
#1604=FACE_OUTER_BOUND('',#2400,.T.);
#1605=FACE_OUTER_BOUND('',#2401,.T.);
#1606=FACE_OUTER_BOUND('',#2402,.T.);
#1607=FACE_OUTER_BOUND('',#2403,.T.);
#1608=FACE_OUTER_BOUND('',#2404,.T.);
#1609=FACE_OUTER_BOUND('',#2405,.T.);
#1610=FACE_OUTER_BOUND('',#2406,.T.);
#1611=FACE_OUTER_BOUND('',#2408,.T.);
#1612=FACE_OUTER_BOUND('',#2410,.T.);
#1613=FACE_OUTER_BOUND('',#2411,.T.);
#1614=FACE_OUTER_BOUND('',#2412,.T.);
#1615=FACE_OUTER_BOUND('',#2413,.T.);
#1616=FACE_OUTER_BOUND('',#2414,.T.);
#1617=FACE_OUTER_BOUND('',#2415,.T.);
#1618=FACE_OUTER_BOUND('',#2416,.T.);
#1619=FACE_OUTER_BOUND('',#2417,.T.);
#1620=FACE_OUTER_BOUND('',#2418,.T.);
#1621=FACE_OUTER_BOUND('',#2420,.T.);
#1622=FACE_OUTER_BOUND('',#2422,.T.);
#1623=FACE_OUTER_BOUND('',#2423,.T.);
#1624=FACE_OUTER_BOUND('',#2424,.T.);
#1625=FACE_OUTER_BOUND('',#2425,.T.);
#1626=FACE_OUTER_BOUND('',#2426,.T.);
#1627=FACE_OUTER_BOUND('',#2427,.T.);
#1628=FACE_OUTER_BOUND('',#2428,.T.);
#1629=FACE_OUTER_BOUND('',#2429,.T.);
#1630=FACE_OUTER_BOUND('',#2430,.T.);
#1631=FACE_OUTER_BOUND('',#2432,.T.);
#1632=FACE_OUTER_BOUND('',#2434,.T.);
#1633=FACE_OUTER_BOUND('',#2435,.T.);
#1634=FACE_OUTER_BOUND('',#2436,.T.);
#1635=FACE_OUTER_BOUND('',#2437,.T.);
#1636=FACE_OUTER_BOUND('',#2438,.T.);
#1637=FACE_OUTER_BOUND('',#2439,.T.);
#1638=FACE_OUTER_BOUND('',#2440,.T.);
#1639=FACE_OUTER_BOUND('',#2441,.T.);
#1640=FACE_OUTER_BOUND('',#2442,.T.);
#1641=FACE_OUTER_BOUND('',#2444,.T.);
#1642=FACE_OUTER_BOUND('',#2446,.T.);
#1643=FACE_OUTER_BOUND('',#2447,.T.);
#1644=FACE_OUTER_BOUND('',#2448,.T.);
#1645=FACE_OUTER_BOUND('',#2449,.T.);
#1646=FACE_OUTER_BOUND('',#2450,.T.);
#1647=FACE_OUTER_BOUND('',#2451,.T.);
#1648=FACE_OUTER_BOUND('',#2452,.T.);
#1649=FACE_OUTER_BOUND('',#2453,.T.);
#1650=FACE_OUTER_BOUND('',#2454,.T.);
#1651=FACE_OUTER_BOUND('',#2456,.T.);
#1652=FACE_OUTER_BOUND('',#2458,.T.);
#1653=FACE_OUTER_BOUND('',#2459,.T.);
#1654=FACE_OUTER_BOUND('',#2460,.T.);
#1655=FACE_OUTER_BOUND('',#2461,.T.);
#1656=FACE_OUTER_BOUND('',#2462,.T.);
#1657=FACE_OUTER_BOUND('',#2463,.T.);
#1658=FACE_OUTER_BOUND('',#2464,.T.);
#1659=FACE_OUTER_BOUND('',#2465,.T.);
#2295=EDGE_LOOP('',(#9635,#9636,#9637,#9638));
#2296=EDGE_LOOP('',(#9639,#9640,#9641,#9642,#9643,#9644));
#2297=EDGE_LOOP('',(#9645,#9646,#9647,#9648,#9649));
#2298=EDGE_LOOP('',(#9650,#9651,#9652,#9653,#9654));
#2299=EDGE_LOOP('',(#9655,#9656,#9657,#9658,#9659,#9660));
#2300=EDGE_LOOP('',(#9661,#9662,#9663,#9664));
#2301=EDGE_LOOP('',(#9665,#9666,#9667,#9668));
#2302=EDGE_LOOP('',(#9669,#9670,#9671,#9672));
#2303=EDGE_LOOP('',(#9673));
#2304=EDGE_LOOP('',(#9674));
#2305=EDGE_LOOP('',(#9675));
#2306=EDGE_LOOP('',(#9676));
#2307=EDGE_LOOP('',(#9677,#9678));
#2308=EDGE_LOOP('',(#9679,#9680));
#2309=EDGE_LOOP('',(#9681,#9682));
#2310=EDGE_LOOP('',(#9683,#9684));
#2311=EDGE_LOOP('',(#9685,#9686));
#2312=EDGE_LOOP('',(#9687,#9688));
#2313=EDGE_LOOP('',(#9689,#9690));
#2314=EDGE_LOOP('',(#9691,#9692,#9693,#9694,#9695));
#2315=EDGE_LOOP('',(#9696,#9697,#9698,#9699));
#2316=EDGE_LOOP('',(#9700,#9701,#9702,#9703));
#2317=EDGE_LOOP('',(#9704,#9705,#9706,#9707,#9708));
#2318=EDGE_LOOP('',(#9709,#9710,#9711,#9712));
#2319=EDGE_LOOP('',(#9713,#9714,#9715,#9716,#9717));
#2320=EDGE_LOOP('',(#9718,#9719,#9720,#9721,#9722));
#2321=EDGE_LOOP('',(#9723,#9724,#9725,#9726));
#2322=EDGE_LOOP('',(#9727,#9728,#9729,#9730));
#2323=EDGE_LOOP('',(#9731,#9732,#9733,#9734));
#2324=EDGE_LOOP('',(#9735,#9736,#9737,#9738));
#2325=EDGE_LOOP('',(#9739,#9740,#9741,#9742));
#2326=EDGE_LOOP('',(#9743,#9744,#9745,#9746,#9747));
#2327=EDGE_LOOP('',(#9748,#9749,#9750,#9751,#9752));
#2328=EDGE_LOOP('',(#9753));
#2329=EDGE_LOOP('',(#9754));
#2330=EDGE_LOOP('',(#9755));
#2331=EDGE_LOOP('',(#9756));
#2332=EDGE_LOOP('',(#9757));
#2333=EDGE_LOOP('',(#9758));
#2334=EDGE_LOOP('',(#9759));
#2335=EDGE_LOOP('',(#9760));
#2336=EDGE_LOOP('',(#9761));
#2337=EDGE_LOOP('',(#9762));
#2338=EDGE_LOOP('',(#9763));
#2339=EDGE_LOOP('',(#9764));
#2340=EDGE_LOOP('',(#9765,#9766,#9767,#9768));
#2341=EDGE_LOOP('',(#9769,#9770,#9771,#9772));
#2342=EDGE_LOOP('',(#9773,#9774,#9775,#9776));
#2343=EDGE_LOOP('',(#9777,#9778,#9779,#9780,#9781,#9782,#9783,#9784,#9785,
#9786,#9787,#9788));
#2344=EDGE_LOOP('',(#9789));
#2345=EDGE_LOOP('',(#9790));
#2346=EDGE_LOOP('',(#9791,#9792,#9793,#9794));
#2347=EDGE_LOOP('',(#9795,#9796,#9797,#9798));
#2348=EDGE_LOOP('',(#9799,#9800,#9801,#9802));
#2349=EDGE_LOOP('',(#9803,#9804,#9805,#9806,#9807,#9808,#9809,#9810,#9811,
#9812,#9813,#9814));
#2350=EDGE_LOOP('',(#9815));
#2351=EDGE_LOOP('',(#9816));
#2352=EDGE_LOOP('',(#9817,#9818,#9819,#9820));
#2353=EDGE_LOOP('',(#9821,#9822,#9823,#9824));
#2354=EDGE_LOOP('',(#9825,#9826,#9827,#9828));
#2355=EDGE_LOOP('',(#9829,#9830,#9831,#9832,#9833,#9834,#9835,#9836,#9837,
#9838,#9839,#9840));
#2356=EDGE_LOOP('',(#9841));
#2357=EDGE_LOOP('',(#9842));
#2358=EDGE_LOOP('',(#9843,#9844,#9845,#9846));
#2359=EDGE_LOOP('',(#9847,#9848,#9849,#9850));
#2360=EDGE_LOOP('',(#9851,#9852,#9853,#9854));
#2361=EDGE_LOOP('',(#9855,#9856,#9857,#9858,#9859,#9860,#9861,#9862,#9863,
#9864,#9865,#9866));
#2362=EDGE_LOOP('',(#9867));
#2363=EDGE_LOOP('',(#9868));
#2364=EDGE_LOOP('',(#9869,#9870,#9871,#9872));
#2365=EDGE_LOOP('',(#9873,#9874,#9875,#9876));
#2366=EDGE_LOOP('',(#9877,#9878,#9879,#9880));
#2367=EDGE_LOOP('',(#9881,#9882,#9883,#9884,#9885,#9886,#9887,#9888,#9889,
#9890,#9891,#9892));
#2368=EDGE_LOOP('',(#9893));
#2369=EDGE_LOOP('',(#9894));
#2370=EDGE_LOOP('',(#9895,#9896,#9897,#9898));
#2371=EDGE_LOOP('',(#9899,#9900,#9901,#9902));
#2372=EDGE_LOOP('',(#9903,#9904,#9905,#9906));
#2373=EDGE_LOOP('',(#9907,#9908,#9909,#9910,#9911,#9912,#9913,#9914,#9915,
#9916,#9917,#9918));
#2374=EDGE_LOOP('',(#9919));
#2375=EDGE_LOOP('',(#9920));
#2376=EDGE_LOOP('',(#9921,#9922,#9923,#9924,#9925,#9926,#9927,#9928,#9929,
#9930,#9931,#9932));
#2377=EDGE_LOOP('',(#9933));
#2378=EDGE_LOOP('',(#9934));
#2379=EDGE_LOOP('',(#9935,#9936,#9937,#9938));
#2380=EDGE_LOOP('',(#9939,#9940,#9941,#9942));
#2381=EDGE_LOOP('',(#9943,#9944,#9945,#9946));
#2382=EDGE_LOOP('',(#9947,#9948,#9949,#9950));
#2383=EDGE_LOOP('',(#9951,#9952,#9953,#9954));
#2384=EDGE_LOOP('',(#9955,#9956,#9957,#9958));
#2385=EDGE_LOOP('',(#9959,#9960,#9961,#9962));
#2386=EDGE_LOOP('',(#9963));
#2387=EDGE_LOOP('',(#9964));
#2388=EDGE_LOOP('',(#9965));
#2389=EDGE_LOOP('',(#9966));
#2390=EDGE_LOOP('',(#9967,#9968,#9969,#9970));
#2391=EDGE_LOOP('',(#9971,#9972,#9973,#9974,#9975,#9976));
#2392=EDGE_LOOP('',(#9977,#9978,#9979,#9980));
#2393=EDGE_LOOP('',(#9981,#9982,#9983,#9984));
#2394=EDGE_LOOP('',(#9985));
#2395=EDGE_LOOP('',(#9986));
#2396=EDGE_LOOP('',(#9987));
#2397=EDGE_LOOP('',(#9988));
#2398=EDGE_LOOP('',(#9989,#9990,#9991,#9992));
#2399=EDGE_LOOP('',(#9993,#9994,#9995,#9996));
#2400=EDGE_LOOP('',(#9997,#9998,#9999,#10000));
#2401=EDGE_LOOP('',(#10001,#10002,#10003,#10004));
#2402=EDGE_LOOP('',(#10005,#10006,#10007,#10008));
#2403=EDGE_LOOP('',(#10009,#10010,#10011,#10012));
#2404=EDGE_LOOP('',(#10013,#10014,#10015,#10016,#10017,#10018));
#2405=EDGE_LOOP('',(#10019,#10020,#10021,#10022));
#2406=EDGE_LOOP('',(#10023));
#2407=EDGE_LOOP('',(#10024));
#2408=EDGE_LOOP('',(#10025));
#2409=EDGE_LOOP('',(#10026));
#2410=EDGE_LOOP('',(#10027,#10028,#10029,#10030));
#2411=EDGE_LOOP('',(#10031,#10032,#10033,#10034));
#2412=EDGE_LOOP('',(#10035,#10036,#10037,#10038));
#2413=EDGE_LOOP('',(#10039,#10040,#10041,#10042));
#2414=EDGE_LOOP('',(#10043,#10044,#10045,#10046));
#2415=EDGE_LOOP('',(#10047,#10048,#10049,#10050));
#2416=EDGE_LOOP('',(#10051,#10052,#10053,#10054,#10055,#10056));
#2417=EDGE_LOOP('',(#10057,#10058,#10059,#10060));
#2418=EDGE_LOOP('',(#10061));
#2419=EDGE_LOOP('',(#10062));
#2420=EDGE_LOOP('',(#10063));
#2421=EDGE_LOOP('',(#10064));
#2422=EDGE_LOOP('',(#10065,#10066,#10067,#10068));
#2423=EDGE_LOOP('',(#10069,#10070,#10071,#10072));
#2424=EDGE_LOOP('',(#10073,#10074,#10075,#10076));
#2425=EDGE_LOOP('',(#10077,#10078,#10079,#10080));
#2426=EDGE_LOOP('',(#10081,#10082,#10083,#10084));
#2427=EDGE_LOOP('',(#10085,#10086,#10087,#10088));
#2428=EDGE_LOOP('',(#10089,#10090,#10091,#10092,#10093,#10094));
#2429=EDGE_LOOP('',(#10095,#10096,#10097,#10098));
#2430=EDGE_LOOP('',(#10099));
#2431=EDGE_LOOP('',(#10100));
#2432=EDGE_LOOP('',(#10101));
#2433=EDGE_LOOP('',(#10102));
#2434=EDGE_LOOP('',(#10103,#10104,#10105,#10106));
#2435=EDGE_LOOP('',(#10107,#10108,#10109,#10110));
#2436=EDGE_LOOP('',(#10111,#10112,#10113,#10114));
#2437=EDGE_LOOP('',(#10115,#10116,#10117,#10118));
#2438=EDGE_LOOP('',(#10119,#10120,#10121,#10122));
#2439=EDGE_LOOP('',(#10123,#10124,#10125,#10126));
#2440=EDGE_LOOP('',(#10127,#10128,#10129,#10130,#10131,#10132));
#2441=EDGE_LOOP('',(#10133,#10134,#10135,#10136));
#2442=EDGE_LOOP('',(#10137));
#2443=EDGE_LOOP('',(#10138));
#2444=EDGE_LOOP('',(#10139));
#2445=EDGE_LOOP('',(#10140));
#2446=EDGE_LOOP('',(#10141,#10142,#10143,#10144));
#2447=EDGE_LOOP('',(#10145,#10146,#10147,#10148));
#2448=EDGE_LOOP('',(#10149,#10150,#10151,#10152));
#2449=EDGE_LOOP('',(#10153,#10154,#10155,#10156));
#2450=EDGE_LOOP('',(#10157,#10158,#10159,#10160));
#2451=EDGE_LOOP('',(#10161,#10162,#10163,#10164));
#2452=EDGE_LOOP('',(#10165,#10166,#10167,#10168,#10169,#10170));
#2453=EDGE_LOOP('',(#10171,#10172,#10173,#10174));
#2454=EDGE_LOOP('',(#10175));
#2455=EDGE_LOOP('',(#10176));
#2456=EDGE_LOOP('',(#10177));
#2457=EDGE_LOOP('',(#10178));
#2458=EDGE_LOOP('',(#10179,#10180,#10181,#10182));
#2459=EDGE_LOOP('',(#10183,#10184,#10185,#10186));
#2460=EDGE_LOOP('',(#10187,#10188,#10189,#10190));
#2461=EDGE_LOOP('',(#10191,#10192,#10193,#10194));
#2462=EDGE_LOOP('',(#10195,#10196,#10197,#10198));
#2463=EDGE_LOOP('',(#10199,#10200,#10201,#10202,#10203,#10204));
#2464=EDGE_LOOP('',(#10205,#10206,#10207,#10208));
#2465=EDGE_LOOP('',(#10209,#10210,#10211,#10212));
#3367=LINE('',#38051,#3815);
#3368=LINE('',#38054,#3816);
#3369=LINE('',#38057,#3817);
#3370=LINE('',#38061,#3818);
#3371=LINE('',#38066,#3819);
#3372=LINE('',#38129,#3820);
#3373=LINE('',#38134,#3821);
#3374=LINE('',#38137,#3822);
#3375=LINE('',#38144,#3823);
#3376=LINE('',#38147,#3824);
#3377=LINE('',#38153,#3825);
#3378=LINE('',#38159,#3826);
#3379=LINE('',#38166,#3827);
#3380=LINE('',#38170,#3828);
#3815=VECTOR('',#16197,8.14999999999999);
#3816=VECTOR('',#16202,7.5);
#3817=VECTOR('',#16205,7.5);
#3818=VECTOR('',#16210,12.4653846153846);
#3819=VECTOR('',#16217,12.4653846153846);
#3820=VECTOR('',#16290,17.6897435897436);
#3821=VECTOR('',#16297,16.2686153846154);
#3822=VECTOR('',#16300,16.0346153846154);
#3823=VECTOR('',#16311,16.0346153846154);
#3824=VECTOR('',#16314,16.2686153846154);
#3825=VECTOR('',#16321,17.6897435897436);
#3826=VECTOR('',#16328,20.35);
#3827=VECTOR('',#16335,21.);
#3828=VECTOR('',#16342,21.);
#4147=CIRCLE('',#13629,12.4653846153846);
#4148=CIRCLE('',#13630,3.56616156686793);
#4149=CIRCLE('',#13631,12.4653846153846);
#4150=CIRCLE('',#13633,7.64278544417155);
#4151=CIRCLE('',#13634,7.64278544417155);
#4152=CIRCLE('',#13635,0.4875);
#4153=CIRCLE('',#13636,7.5);
#4154=CIRCLE('',#13637,7.5);
#4155=CIRCLE('',#13639,7.5);
#4156=CIRCLE('',#13640,7.5);
#4157=CIRCLE('',#13641,0.4875);
#4158=CIRCLE('',#13642,7.64278544417155);
#4159=CIRCLE('',#13644,8.14999999999999);
#4160=CIRCLE('',#13647,8.14999999999999);
#4161=CIRCLE('',#13649,12.4653846153846);
#4162=CIRCLE('',#13651,12.4653846153846);
#4163=CIRCLE('',#13655,3.56616156686793);
#4164=CIRCLE('',#13657,3.56616156686793);
#4165=CIRCLE('',#13659,3.56616156686793);
#4166=CIRCLE('',#13661,3.56616156686793);
#4167=CIRCLE('',#13663,3.56616156686793);
#4168=CIRCLE('',#13665,3.56616156686793);
#4169=CIRCLE('',#13667,3.56616156686793);
#4170=CIRCLE('',#13669,16.3271153846154);
#4171=CIRCLE('',#13670,0.0585);
#4172=CIRCLE('',#13671,16.2686153846154);
#4173=CIRCLE('',#13672,16.2686153846154);
#4174=CIRCLE('',#13674,16.0346153846154);
#4175=CIRCLE('',#13675,0.0585);
#4176=CIRCLE('',#13676,16.0931153846154);
#4177=CIRCLE('',#13678,16.3271153846154);
#4178=CIRCLE('',#13679,0.0585);
#4179=CIRCLE('',#13680,16.2686153846154);
#4180=CIRCLE('',#13682,16.0346153846154);
#4181=CIRCLE('',#13683,16.0346153846154);
#4182=CIRCLE('',#13684,0.0585);
#4183=CIRCLE('',#13685,16.0931153846154);
#4184=CIRCLE('',#13687,17.6897435897436);
#4185=CIRCLE('',#13688,17.6897435897436);
#4186=CIRCLE('',#13690,16.2686153846154);
#4187=CIRCLE('',#13692,16.0346153846154);
#4188=CIRCLE('',#13694,3.56616156686793);
#4189=CIRCLE('',#13695,16.0346153846154);
#4190=CIRCLE('',#13698,16.2686153846154);
#4191=CIRCLE('',#13700,17.6897435897436);
#4192=CIRCLE('',#13701,17.6897435897436);
#4193=CIRCLE('',#13703,21.);
#4194=CIRCLE('',#13704,20.35);
#4195=CIRCLE('',#13706,21.);
#4196=CIRCLE('',#13707,20.35);
#4197=CIRCLE('',#13708,21.);
#4198=CIRCLE('',#13717,3.96060240207311);
#4199=CIRCLE('',#13718,1.69469015025);
#4200=CIRCLE('',#13719,3.96060240207311);
#4201=CIRCLE('',#13721,3.39763111739558);
#4202=CIRCLE('',#13722,3.56616156686792);
#4203=CIRCLE('',#13723,3.39763111739558);
#4204=CIRCLE('',#13724,3.39763111739558);
#4205=CIRCLE('',#13725,3.39763111739558);
#4206=CIRCLE('',#13726,3.39763111739558);
#4207=CIRCLE('',#13727,3.39763111739558);
#4208=CIRCLE('',#13728,3.45272288248773);
#4209=CIRCLE('',#13729,3.45272288248773);
#4210=CIRCLE('',#13731,3.96060240207311);
#4211=CIRCLE('',#13732,1.69469015025);
#4212=CIRCLE('',#13733,3.96060240207311);
#4213=CIRCLE('',#13735,3.39763111739558);
#4214=CIRCLE('',#13736,3.56616156686792);
#4215=CIRCLE('',#13737,3.39763111739558);
#4216=CIRCLE('',#13738,3.39763111739558);
#4217=CIRCLE('',#13739,3.39763111739558);
#4218=CIRCLE('',#13740,3.39763111739558);
#4219=CIRCLE('',#13741,3.39763111739558);
#4220=CIRCLE('',#13742,3.45272288248773);
#4221=CIRCLE('',#13743,3.45272288248773);
#4222=CIRCLE('',#13745,3.96060240207311);
#4223=CIRCLE('',#13746,1.69469015025);
#4224=CIRCLE('',#13747,3.96060240207311);
#4225=CIRCLE('',#13749,3.39763111739558);
#4226=CIRCLE('',#13750,3.56616156686792);
#4227=CIRCLE('',#13751,3.39763111739558);
#4228=CIRCLE('',#13752,3.39763111739558);
#4229=CIRCLE('',#13753,3.39763111739558);
#4230=CIRCLE('',#13754,3.39763111739558);
#4231=CIRCLE('',#13755,3.39763111739558);
#4232=CIRCLE('',#13756,3.45272288248773);
#4233=CIRCLE('',#13757,3.45272288248773);
#4234=CIRCLE('',#13759,3.96060240207311);
#4235=CIRCLE('',#13760,1.69469015025);
#4236=CIRCLE('',#13761,3.96060240207311);
#4237=CIRCLE('',#13763,3.39763111739558);
#4238=CIRCLE('',#13764,3.56616156686792);
#4239=CIRCLE('',#13765,3.39763111739558);
#4240=CIRCLE('',#13766,3.39763111739558);
#4241=CIRCLE('',#13767,3.39763111739558);
#4242=CIRCLE('',#13768,3.39763111739558);
#4243=CIRCLE('',#13769,3.39763111739558);
#4244=CIRCLE('',#13770,3.45272288248773);
#4245=CIRCLE('',#13771,3.45272288248773);
#4246=CIRCLE('',#13773,3.96060240207311);
#4247=CIRCLE('',#13774,1.69469015025);
#4248=CIRCLE('',#13775,3.96060240207311);
#4249=CIRCLE('',#13777,3.39763111739558);
#4250=CIRCLE('',#13778,3.56616156686792);
#4251=CIRCLE('',#13779,3.39763111739558);
#4252=CIRCLE('',#13780,3.39763111739558);
#4253=CIRCLE('',#13781,3.39763111739558);
#4254=CIRCLE('',#13782,3.39763111739558);
#4255=CIRCLE('',#13783,3.39763111739558);
#4256=CIRCLE('',#13784,3.45272288248773);
#4257=CIRCLE('',#13785,3.45272288248773);
#4258=CIRCLE('',#13787,3.96060240207311);
#4259=CIRCLE('',#13788,1.69469015025);
#4260=CIRCLE('',#13789,3.96060240207311);
#4261=CIRCLE('',#13791,3.39763111739558);
#4262=CIRCLE('',#13792,3.39763111739558);
#4263=CIRCLE('',#13793,3.39763111739558);
#4264=CIRCLE('',#13794,3.56616156686792);
#4265=CIRCLE('',#13795,3.39763111739558);
#4266=CIRCLE('',#13796,3.39763111739558);
#4267=CIRCLE('',#13797,3.39763111739558);
#4268=CIRCLE('',#13798,3.45272288248773);
#4269=CIRCLE('',#13799,3.45272288248773);
#4270=CIRCLE('',#13801,3.39763111739558);
#4271=CIRCLE('',#13802,3.56616156686792);
#4272=CIRCLE('',#13803,3.39763111739558);
#4273=CIRCLE('',#13804,3.39763111739558);
#4274=CIRCLE('',#13805,3.39763111739558);
#4275=CIRCLE('',#13806,3.39763111739558);
#4276=CIRCLE('',#13807,3.39763111739558);
#4277=CIRCLE('',#13808,3.45272288248773);
#4278=CIRCLE('',#13809,3.45272288248773);
#4279=CIRCLE('',#13811,3.96060240207311);
#4280=CIRCLE('',#13812,1.69469015025);
#4281=CIRCLE('',#13813,3.96060240207311);
#4282=CIRCLE('',#13815,14.25);
#4283=CIRCLE('',#13816,14.25);
#4284=CIRCLE('',#13818,15.1423076923077);
#4285=CIRCLE('',#13819,15.1423076923077);
#4286=CIRCLE('',#13825,14.25);
#4287=CIRCLE('',#13826,15.1423076923077);
#4288=CIRCLE('',#13828,14.25);
#4289=CIRCLE('',#13829,15.1423076923077);
#4290=CIRCLE('',#13835,14.25);
#4291=CIRCLE('',#13836,15.1423076923077);
#4292=CIRCLE('',#13838,14.25);
#4293=CIRCLE('',#13839,15.1423076923077);
#4294=CIRCLE('',#13843,14.25);
#4295=CIRCLE('',#13844,14.25);
#4296=CIRCLE('',#13846,15.1423076923077);
#4297=CIRCLE('',#13847,15.1423076923077);
#4298=CIRCLE('',#13853,14.25);
#4299=CIRCLE('',#13854,15.1423076923077);
#4300=CIRCLE('',#13856,14.25);
#4301=CIRCLE('',#13857,15.1423076923077);
#4302=CIRCLE('',#13861,14.25);
#4303=CIRCLE('',#13862,14.25);
#4304=CIRCLE('',#13864,15.1423076923077);
#4305=CIRCLE('',#13865,15.1423076923077);
#4306=CIRCLE('',#13871,14.25);
#4307=CIRCLE('',#13872,15.1423076923077);
#4308=CIRCLE('',#13874,14.25);
#4309=CIRCLE('',#13875,15.1423076923077);
#4310=CIRCLE('',#13879,14.25);
#4311=CIRCLE('',#13880,14.25);
#4312=CIRCLE('',#13882,15.1423076923077);
#4313=CIRCLE('',#13883,15.1423076923077);
#4314=CIRCLE('',#13889,14.25);
#4315=CIRCLE('',#13890,15.1423076923077);
#4316=CIRCLE('',#13892,14.25);
#4317=CIRCLE('',#13893,15.1423076923077);
#4318=CIRCLE('',#13897,14.25);
#4319=CIRCLE('',#13898,14.25);
#4320=CIRCLE('',#13900,15.1423076923077);
#4321=CIRCLE('',#13901,15.1423076923077);
#4322=CIRCLE('',#13907,14.25);
#4323=CIRCLE('',#13908,15.1423076923077);
#4324=CIRCLE('',#13910,14.25);
#4325=CIRCLE('',#13911,15.1423076923077);
#4326=CIRCLE('',#13915,14.25);
#4327=CIRCLE('',#13916,14.25);
#4328=CIRCLE('',#13918,15.1423076923077);
#4329=CIRCLE('',#13919,15.1423076923077);
#4330=CIRCLE('',#13925,14.25);
#4331=CIRCLE('',#13926,15.1423076923077);
#4332=CIRCLE('',#13928,14.25);
#4333=CIRCLE('',#13929,15.1423076923077);
#4334=CIRCLE('',#13933,14.25);
#4335=CIRCLE('',#13934,15.1423076923077);
#4336=CIRCLE('',#13936,14.25);
#4337=CIRCLE('',#13937,15.1423076923077);
#5407=VERTEX_POINT('',#38026);
#5408=VERTEX_POINT('',#38028);
#5409=VERTEX_POINT('',#38032);
#5410=VERTEX_POINT('',#38033);
#5411=VERTEX_POINT('',#38036);
#5412=VERTEX_POINT('',#38038);
#5413=VERTEX_POINT('',#38042);
#5414=VERTEX_POINT('',#38043);
#5415=VERTEX_POINT('',#38046);
#5416=VERTEX_POINT('',#38050);
#5417=VERTEX_POINT('',#38056);
#5418=VERTEX_POINT('',#38060);
#5419=VERTEX_POINT('',#38064);
#5420=VERTEX_POINT('',#38070);
#5421=VERTEX_POINT('',#38071);
#5422=VERTEX_POINT('',#38074);
#5423=VERTEX_POINT('',#38075);
#5424=VERTEX_POINT('',#38078);
#5425=VERTEX_POINT('',#38079);
#5426=VERTEX_POINT('',#38082);
#5427=VERTEX_POINT('',#38083);
#5428=VERTEX_POINT('',#38086);
#5429=VERTEX_POINT('',#38087);
#5430=VERTEX_POINT('',#38090);
#5431=VERTEX_POINT('',#38091);
#5432=VERTEX_POINT('',#38094);
#5433=VERTEX_POINT('',#38095);
#5434=VERTEX_POINT('',#38098);
#5435=VERTEX_POINT('',#38100);
#5436=VERTEX_POINT('',#38102);
#5437=VERTEX_POINT('',#38106);
#5438=VERTEX_POINT('',#38108);
#5439=VERTEX_POINT('',#38112);
#5440=VERTEX_POINT('',#38114);
#5441=VERTEX_POINT('',#38118);
#5442=VERTEX_POINT('',#38119);
#5443=VERTEX_POINT('',#38122);
#5444=VERTEX_POINT('',#38126);
#5445=VERTEX_POINT('',#38128);
#5446=VERTEX_POINT('',#38132);
#5447=VERTEX_POINT('',#38136);
#5448=VERTEX_POINT('',#38140);
#5449=VERTEX_POINT('',#38146);
#5450=VERTEX_POINT('',#38150);
#5451=VERTEX_POINT('',#38152);
#5452=VERTEX_POINT('',#38156);
#5453=VERTEX_POINT('',#38158);
#5454=VERTEX_POINT('',#38162);
#5455=VERTEX_POINT('',#38163);
#5456=VERTEX_POINT('',#38165);
#5457=VERTEX_POINT('',#38178);
#5458=VERTEX_POINT('',#38180);
#5459=VERTEX_POINT('',#38183);
#5460=VERTEX_POINT('',#38184);
#5461=VERTEX_POINT('',#38191);
#5462=VERTEX_POINT('',#38211);
#5463=VERTEX_POINT('',#38237);
#5464=VERTEX_POINT('',#38238);
#5465=VERTEX_POINT('',#38245);
#5466=VERTEX_POINT('',#38265);
#5467=VERTEX_POINT('',#38292);
#5468=VERTEX_POINT('',#38293);
#5469=VERTEX_POINT('',#38295);
#5470=VERTEX_POINT('',#38297);
#5471=VERTEX_POINT('',#38299);
#5472=VERTEX_POINT('',#38307);
#5473=VERTEX_POINT('',#38309);
#5474=VERTEX_POINT('',#38318);
#5475=VERTEX_POINT('',#38320);
#5476=VERTEX_POINT('',#38327);
#5477=VERTEX_POINT('',#38335);
#5478=VERTEX_POINT('',#38337);
#5479=VERTEX_POINT('',#38340);
#5480=VERTEX_POINT('',#38342);
#5481=VERTEX_POINT('',#38345);
#5482=VERTEX_POINT('',#38346);
#5483=VERTEX_POINT('',#38353);
#5484=VERTEX_POINT('',#38373);
#5485=VERTEX_POINT('',#38399);
#5486=VERTEX_POINT('',#38400);
#5487=VERTEX_POINT('',#38407);
#5488=VERTEX_POINT('',#38427);
#5489=VERTEX_POINT('',#38454);
#5490=VERTEX_POINT('',#38455);
#5491=VERTEX_POINT('',#38457);
#5492=VERTEX_POINT('',#38459);
#5493=VERTEX_POINT('',#38461);
#5494=VERTEX_POINT('',#38469);
#5495=VERTEX_POINT('',#38471);
#5496=VERTEX_POINT('',#38480);
#5497=VERTEX_POINT('',#38482);
#5498=VERTEX_POINT('',#38489);
#5499=VERTEX_POINT('',#38497);
#5500=VERTEX_POINT('',#38499);
#5501=VERTEX_POINT('',#38502);
#5502=VERTEX_POINT('',#38504);
#5503=VERTEX_POINT('',#38507);
#5504=VERTEX_POINT('',#38508);
#5505=VERTEX_POINT('',#38515);
#5506=VERTEX_POINT('',#38535);
#5507=VERTEX_POINT('',#38561);
#5508=VERTEX_POINT('',#38562);
#5509=VERTEX_POINT('',#38569);
#5510=VERTEX_POINT('',#38589);
#5511=VERTEX_POINT('',#38616);
#5512=VERTEX_POINT('',#38617);
#5513=VERTEX_POINT('',#38619);
#5514=VERTEX_POINT('',#38621);
#5515=VERTEX_POINT('',#38623);
#5516=VERTEX_POINT('',#38631);
#5517=VERTEX_POINT('',#38633);
#5518=VERTEX_POINT('',#38642);
#5519=VERTEX_POINT('',#38644);
#5520=VERTEX_POINT('',#38651);
#5521=VERTEX_POINT('',#38659);
#5522=VERTEX_POINT('',#38661);
#5523=VERTEX_POINT('',#38664);
#5524=VERTEX_POINT('',#38666);
#5525=VERTEX_POINT('',#38669);
#5526=VERTEX_POINT('',#38670);
#5527=VERTEX_POINT('',#38677);
#5528=VERTEX_POINT('',#38697);
#5529=VERTEX_POINT('',#38723);
#5530=VERTEX_POINT('',#38724);
#5531=VERTEX_POINT('',#38731);
#5532=VERTEX_POINT('',#38751);
#5533=VERTEX_POINT('',#38778);
#5534=VERTEX_POINT('',#38779);
#5535=VERTEX_POINT('',#38781);
#5536=VERTEX_POINT('',#38783);
#5537=VERTEX_POINT('',#38785);
#5538=VERTEX_POINT('',#38793);
#5539=VERTEX_POINT('',#38795);
#5540=VERTEX_POINT('',#38804);
#5541=VERTEX_POINT('',#38806);
#5542=VERTEX_POINT('',#38813);
#5543=VERTEX_POINT('',#38821);
#5544=VERTEX_POINT('',#38823);
#5545=VERTEX_POINT('',#38826);
#5546=VERTEX_POINT('',#38828);
#5547=VERTEX_POINT('',#38831);
#5548=VERTEX_POINT('',#38832);
#5549=VERTEX_POINT('',#38839);
#5550=VERTEX_POINT('',#38859);
#5551=VERTEX_POINT('',#38885);
#5552=VERTEX_POINT('',#38886);
#5553=VERTEX_POINT('',#38893);
#5554=VERTEX_POINT('',#38913);
#5555=VERTEX_POINT('',#38940);
#5556=VERTEX_POINT('',#38941);
#5557=VERTEX_POINT('',#38943);
#5558=VERTEX_POINT('',#38945);
#5559=VERTEX_POINT('',#38947);
#5560=VERTEX_POINT('',#38955);
#5561=VERTEX_POINT('',#38957);
#5562=VERTEX_POINT('',#38966);
#5563=VERTEX_POINT('',#38968);
#5564=VERTEX_POINT('',#38975);
#5565=VERTEX_POINT('',#38983);
#5566=VERTEX_POINT('',#38985);
#5567=VERTEX_POINT('',#38988);
#5568=VERTEX_POINT('',#38990);
#5569=VERTEX_POINT('',#38993);
#5570=VERTEX_POINT('',#38994);
#5571=VERTEX_POINT('',#39014);
#5572=VERTEX_POINT('',#39021);
#5573=VERTEX_POINT('',#39047);
#5574=VERTEX_POINT('',#39048);
#5575=VERTEX_POINT('',#39055);
#5576=VERTEX_POINT('',#39075);
#5577=VERTEX_POINT('',#39102);
#5578=VERTEX_POINT('',#39103);
#5579=VERTEX_POINT('',#39105);
#5580=VERTEX_POINT('',#39112);
#5581=VERTEX_POINT('',#39114);
#5582=VERTEX_POINT('',#39122);
#5583=VERTEX_POINT('',#39124);
#5584=VERTEX_POINT('',#39126);
#5585=VERTEX_POINT('',#39134);
#5586=VERTEX_POINT('',#39136);
#5587=VERTEX_POINT('',#39145);
#5588=VERTEX_POINT('',#39147);
#5589=VERTEX_POINT('',#39150);
#5590=VERTEX_POINT('',#39151);
#5591=VERTEX_POINT('',#39153);
#5592=VERTEX_POINT('',#39155);
#5593=VERTEX_POINT('',#39157);
#5594=VERTEX_POINT('',#39165);
#5595=VERTEX_POINT('',#39167);
#5596=VERTEX_POINT('',#39176);
#5597=VERTEX_POINT('',#39178);
#5598=VERTEX_POINT('',#39185);
#5599=VERTEX_POINT('',#39193);
#5600=VERTEX_POINT('',#39195);
#5601=VERTEX_POINT('',#39198);
#5602=VERTEX_POINT('',#39200);
#5603=VERTEX_POINT('',#39203);
#5604=VERTEX_POINT('',#39204);
#5605=VERTEX_POINT('',#39211);
#5606=VERTEX_POINT('',#39231);
#5607=VERTEX_POINT('',#39257);
#5608=VERTEX_POINT('',#39258);
#5609=VERTEX_POINT('',#39265);
#5610=VERTEX_POINT('',#39285);
#6979=EDGE_CURVE('',#5407,#5407,#4147,.T.);
#6980=EDGE_CURVE('',#5407,#5408,#4148,.T.);
#6981=EDGE_CURVE('',#5408,#5408,#4149,.T.);
#6982=EDGE_CURVE('',#5409,#5410,#4150,.T.);
#6983=EDGE_CURVE('',#5410,#5409,#4151,.T.);
#6984=EDGE_CURVE('',#5410,#5411,#4152,.T.);
#6985=EDGE_CURVE('',#5412,#5411,#4153,.T.);
#6986=EDGE_CURVE('',#5411,#5412,#4154,.T.);
#6987=EDGE_CURVE('',#5413,#5414,#4155,.T.);
#6988=EDGE_CURVE('',#5414,#5413,#4156,.T.);
#6989=EDGE_CURVE('',#5414,#5415,#4157,.T.);
#6990=EDGE_CURVE('',#5415,#5415,#4158,.T.);
#6991=EDGE_CURVE('',#5409,#5416,#3367,.T.);
#6992=EDGE_CURVE('',#5416,#5416,#4159,.T.);
#6993=EDGE_CURVE('',#5413,#5412,#3368,.T.);
#6994=EDGE_CURVE('',#5415,#5417,#3369,.T.);
#6995=EDGE_CURVE('',#5417,#5417,#4160,.T.);
#6996=EDGE_CURVE('',#5408,#5418,#3370,.T.);
#6997=EDGE_CURVE('',#5418,#5418,#4161,.T.);
#6998=EDGE_CURVE('',#5419,#5419,#4162,.T.);
#6999=EDGE_CURVE('',#5419,#5407,#3371,.T.);
#7000=EDGE_CURVE('',#5420,#5421,#4163,.T.);
#7001=EDGE_CURVE('',#5422,#5423,#4164,.T.);
#7002=EDGE_CURVE('',#5424,#5425,#4165,.T.);
#7003=EDGE_CURVE('',#5426,#5427,#4166,.T.);
#7004=EDGE_CURVE('',#5428,#5429,#4167,.T.);
#7005=EDGE_CURVE('',#5430,#5431,#4168,.T.);
#7006=EDGE_CURVE('',#5432,#5433,#4169,.T.);
#7007=EDGE_CURVE('',#5434,#5434,#4170,.T.);
#7008=EDGE_CURVE('',#5434,#5435,#4171,.T.);
#7009=EDGE_CURVE('',#5436,#5435,#4172,.T.);
#7010=EDGE_CURVE('',#5435,#5436,#4173,.T.);
#7011=EDGE_CURVE('',#5437,#5437,#4174,.T.);
#7012=EDGE_CURVE('',#5437,#5438,#4175,.T.);
#7013=EDGE_CURVE('',#5438,#5438,#4176,.T.);
#7014=EDGE_CURVE('',#5439,#5439,#4177,.T.);
#7015=EDGE_CURVE('',#5439,#5440,#4178,.T.);
#7016=EDGE_CURVE('',#5440,#5440,#4179,.T.);
#7017=EDGE_CURVE('',#5441,#5442,#4180,.T.);
#7018=EDGE_CURVE('',#5442,#5441,#4181,.T.);
#7019=EDGE_CURVE('',#5442,#5443,#4182,.T.);
#7020=EDGE_CURVE('',#5443,#5443,#4183,.T.);
#7021=EDGE_CURVE('',#5444,#5444,#4184,.T.);
#7022=EDGE_CURVE('',#5444,#5445,#3372,.T.);
#7023=EDGE_CURVE('',#5445,#5445,#4185,.T.);
#7024=EDGE_CURVE('',#5446,#5446,#4186,.T.);
#7025=EDGE_CURVE('',#5446,#5436,#3373,.T.);
#7026=EDGE_CURVE('',#5441,#5447,#3374,.T.);
#7027=EDGE_CURVE('',#5447,#5447,#4187,.T.);
#7028=EDGE_CURVE('',#5447,#5448,#4188,.T.);
#7029=EDGE_CURVE('',#5448,#5448,#4189,.T.);
#7030=EDGE_CURVE('',#5448,#5437,#3375,.T.);
#7031=EDGE_CURVE('',#5440,#5449,#3376,.T.);
#7032=EDGE_CURVE('',#5449,#5449,#4190,.T.);
#7033=EDGE_CURVE('',#5450,#5450,#4191,.T.);
#7034=EDGE_CURVE('',#5450,#5451,#3377,.T.);
#7035=EDGE_CURVE('',#5451,#5451,#4192,.T.);
#7036=EDGE_CURVE('',#5452,#5452,#4193,.T.);
#7037=EDGE_CURVE('',#5452,#5453,#3378,.T.);
#7038=EDGE_CURVE('',#5453,#5453,#4194,.T.);
#7039=EDGE_CURVE('',#5454,#5455,#4195,.T.);
#7040=EDGE_CURVE('',#5455,#5456,#3379,.T.);
#7041=EDGE_CURVE('',#5456,#5456,#4196,.T.);
#7042=EDGE_CURVE('',#5455,#5454,#4197,.T.);
#7043=EDGE_CURVE('',#5454,#5452,#3380,.T.);
#7044=EDGE_CURVE('',#5457,#5457,#4198,.T.);
#7045=EDGE_CURVE('',#5457,#5458,#4199,.T.);
#7046=EDGE_CURVE('',#5458,#5458,#4200,.T.);
#7047=EDGE_CURVE('',#5459,#5460,#611,.T.);
#7048=EDGE_CURVE('',#5459,#5461,#612,.T.);
#7049=EDGE_CURVE('',#5461,#5462,#613,.T.);
#7050=EDGE_CURVE('',#5462,#5460,#614,.T.);
#7051=EDGE_CURVE('',#5463,#5464,#615,.T.);
#7052=EDGE_CURVE('',#5463,#5465,#616,.T.);
#7053=EDGE_CURVE('',#5465,#5466,#617,.T.);
#7054=EDGE_CURVE('',#5466,#5464,#618,.T.);
#7055=EDGE_CURVE('',#5467,#5468,#4201,.T.);
#7056=EDGE_CURVE('',#5468,#5469,#4202,.T.);
#7057=EDGE_CURVE('',#5469,#5470,#4203,.T.);
#7058=EDGE_CURVE('',#5470,#5471,#619,.T.);
#7059=EDGE_CURVE('',#5472,#5471,#4204,.T.);
#7060=EDGE_CURVE('',#5472,#5473,#620,.T.);
#7061=EDGE_CURVE('',#5473,#5469,#4205,.T.);
#7062=EDGE_CURVE('',#5468,#5474,#4206,.T.);
#7063=EDGE_CURVE('',#5474,#5475,#621,.T.);
#7064=EDGE_CURVE('',#5476,#5475,#4207,.T.);
#7065=EDGE_CURVE('',#5476,#5467,#622,.T.);
#7066=EDGE_CURVE('',#5477,#5477,#4208,.T.);
#7067=EDGE_CURVE('',#5478,#5478,#4209,.T.);
#7068=EDGE_CURVE('',#5479,#5479,#4210,.T.);
#7069=EDGE_CURVE('',#5479,#5480,#4211,.T.);
#7070=EDGE_CURVE('',#5480,#5480,#4212,.T.);
#7071=EDGE_CURVE('',#5481,#5482,#623,.T.);
#7072=EDGE_CURVE('',#5481,#5483,#624,.T.);
#7073=EDGE_CURVE('',#5483,#5484,#625,.T.);
#7074=EDGE_CURVE('',#5484,#5482,#626,.T.);
#7075=EDGE_CURVE('',#5485,#5486,#627,.T.);
#7076=EDGE_CURVE('',#5485,#5487,#628,.T.);
#7077=EDGE_CURVE('',#5487,#5488,#629,.T.);
#7078=EDGE_CURVE('',#5488,#5486,#630,.T.);
#7079=EDGE_CURVE('',#5489,#5490,#4213,.T.);
#7080=EDGE_CURVE('',#5490,#5491,#4214,.T.);
#7081=EDGE_CURVE('',#5491,#5492,#4215,.T.);
#7082=EDGE_CURVE('',#5492,#5493,#631,.T.);
#7083=EDGE_CURVE('',#5494,#5493,#4216,.T.);
#7084=EDGE_CURVE('',#5494,#5495,#632,.T.);
#7085=EDGE_CURVE('',#5495,#5491,#4217,.T.);
#7086=EDGE_CURVE('',#5490,#5496,#4218,.T.);
#7087=EDGE_CURVE('',#5496,#5497,#633,.T.);
#7088=EDGE_CURVE('',#5498,#5497,#4219,.T.);
#7089=EDGE_CURVE('',#5498,#5489,#634,.T.);
#7090=EDGE_CURVE('',#5499,#5499,#4220,.T.);
#7091=EDGE_CURVE('',#5500,#5500,#4221,.T.);
#7092=EDGE_CURVE('',#5501,#5501,#4222,.T.);
#7093=EDGE_CURVE('',#5501,#5502,#4223,.T.);
#7094=EDGE_CURVE('',#5502,#5502,#4224,.T.);
#7095=EDGE_CURVE('',#5503,#5504,#635,.T.);
#7096=EDGE_CURVE('',#5503,#5505,#636,.T.);
#7097=EDGE_CURVE('',#5505,#5506,#637,.T.);
#7098=EDGE_CURVE('',#5506,#5504,#638,.T.);
#7099=EDGE_CURVE('',#5507,#5508,#639,.T.);
#7100=EDGE_CURVE('',#5507,#5509,#640,.T.);
#7101=EDGE_CURVE('',#5509,#5510,#641,.T.);
#7102=EDGE_CURVE('',#5510,#5508,#642,.T.);
#7103=EDGE_CURVE('',#5511,#5512,#4225,.T.);
#7104=EDGE_CURVE('',#5512,#5513,#4226,.T.);
#7105=EDGE_CURVE('',#5513,#5514,#4227,.T.);
#7106=EDGE_CURVE('',#5514,#5515,#643,.T.);
#7107=EDGE_CURVE('',#5516,#5515,#4228,.T.);
#7108=EDGE_CURVE('',#5516,#5517,#644,.T.);
#7109=EDGE_CURVE('',#5517,#5513,#4229,.T.);
#7110=EDGE_CURVE('',#5512,#5518,#4230,.T.);
#7111=EDGE_CURVE('',#5518,#5519,#645,.T.);
#7112=EDGE_CURVE('',#5520,#5519,#4231,.T.);
#7113=EDGE_CURVE('',#5520,#5511,#646,.T.);
#7114=EDGE_CURVE('',#5521,#5521,#4232,.T.);
#7115=EDGE_CURVE('',#5522,#5522,#4233,.T.);
#7116=EDGE_CURVE('',#5523,#5523,#4234,.T.);
#7117=EDGE_CURVE('',#5523,#5524,#4235,.T.);
#7118=EDGE_CURVE('',#5524,#5524,#4236,.T.);
#7119=EDGE_CURVE('',#5525,#5526,#647,.T.);
#7120=EDGE_CURVE('',#5525,#5527,#648,.T.);
#7121=EDGE_CURVE('',#5527,#5528,#649,.T.);
#7122=EDGE_CURVE('',#5528,#5526,#650,.T.);
#7123=EDGE_CURVE('',#5529,#5530,#651,.T.);
#7124=EDGE_CURVE('',#5529,#5531,#652,.T.);
#7125=EDGE_CURVE('',#5531,#5532,#653,.T.);
#7126=EDGE_CURVE('',#5532,#5530,#654,.T.);
#7127=EDGE_CURVE('',#5533,#5534,#4237,.T.);
#7128=EDGE_CURVE('',#5534,#5535,#4238,.T.);
#7129=EDGE_CURVE('',#5535,#5536,#4239,.T.);
#7130=EDGE_CURVE('',#5536,#5537,#655,.T.);
#7131=EDGE_CURVE('',#5538,#5537,#4240,.T.);
#7132=EDGE_CURVE('',#5538,#5539,#656,.T.);
#7133=EDGE_CURVE('',#5539,#5535,#4241,.T.);
#7134=EDGE_CURVE('',#5534,#5540,#4242,.T.);
#7135=EDGE_CURVE('',#5540,#5541,#657,.T.);
#7136=EDGE_CURVE('',#5542,#5541,#4243,.T.);
#7137=EDGE_CURVE('',#5542,#5533,#658,.T.);
#7138=EDGE_CURVE('',#5543,#5543,#4244,.T.);
#7139=EDGE_CURVE('',#5544,#5544,#4245,.T.);
#7140=EDGE_CURVE('',#5545,#5545,#4246,.T.);
#7141=EDGE_CURVE('',#5545,#5546,#4247,.T.);
#7142=EDGE_CURVE('',#5546,#5546,#4248,.T.);
#7143=EDGE_CURVE('',#5547,#5548,#659,.T.);
#7144=EDGE_CURVE('',#5547,#5549,#660,.T.);
#7145=EDGE_CURVE('',#5549,#5550,#661,.T.);
#7146=EDGE_CURVE('',#5550,#5548,#662,.T.);
#7147=EDGE_CURVE('',#5551,#5552,#663,.T.);
#7148=EDGE_CURVE('',#5551,#5553,#664,.T.);
#7149=EDGE_CURVE('',#5553,#5554,#665,.T.);
#7150=EDGE_CURVE('',#5554,#5552,#666,.T.);
#7151=EDGE_CURVE('',#5555,#5556,#4249,.T.);
#7152=EDGE_CURVE('',#5556,#5557,#4250,.T.);
#7153=EDGE_CURVE('',#5557,#5558,#4251,.T.);
#7154=EDGE_CURVE('',#5558,#5559,#667,.T.);
#7155=EDGE_CURVE('',#5560,#5559,#4252,.T.);
#7156=EDGE_CURVE('',#5560,#5561,#668,.T.);
#7157=EDGE_CURVE('',#5561,#5557,#4253,.T.);
#7158=EDGE_CURVE('',#5556,#5562,#4254,.T.);
#7159=EDGE_CURVE('',#5562,#5563,#669,.T.);
#7160=EDGE_CURVE('',#5564,#5563,#4255,.T.);
#7161=EDGE_CURVE('',#5564,#5555,#670,.T.);
#7162=EDGE_CURVE('',#5565,#5565,#4256,.T.);
#7163=EDGE_CURVE('',#5566,#5566,#4257,.T.);
#7164=EDGE_CURVE('',#5567,#5567,#4258,.T.);
#7165=EDGE_CURVE('',#5567,#5568,#4259,.T.);
#7166=EDGE_CURVE('',#5568,#5568,#4260,.T.);
#7167=EDGE_CURVE('',#5569,#5570,#671,.T.);
#7168=EDGE_CURVE('',#5569,#5571,#672,.T.);
#7169=EDGE_CURVE('',#5572,#5571,#673,.T.);
#7170=EDGE_CURVE('',#5570,#5572,#674,.T.);
#7171=EDGE_CURVE('',#5573,#5574,#675,.T.);
#7172=EDGE_CURVE('',#5573,#5575,#676,.T.);
#7173=EDGE_CURVE('',#5575,#5576,#677,.T.);
#7174=EDGE_CURVE('',#5576,#5574,#678,.T.);
#7175=EDGE_CURVE('',#5577,#5578,#4261,.T.);
#7176=EDGE_CURVE('',#5579,#5577,#679,.T.);
#7177=EDGE_CURVE('',#5579,#5580,#4262,.T.);
#7178=EDGE_CURVE('',#5581,#5580,#680,.T.);
#7179=EDGE_CURVE('',#5578,#5581,#4263,.T.);
#7180=EDGE_CURVE('',#5578,#5582,#4264,.T.);
#7181=EDGE_CURVE('',#5582,#5583,#4265,.T.);
#7182=EDGE_CURVE('',#5583,#5584,#681,.T.);
#7183=EDGE_CURVE('',#5585,#5584,#4266,.T.);
#7184=EDGE_CURVE('',#5585,#5586,#682,.T.);
#7185=EDGE_CURVE('',#5586,#5582,#4267,.T.);
#7186=EDGE_CURVE('',#5587,#5587,#4268,.T.);
#7187=EDGE_CURVE('',#5588,#5588,#4269,.T.);
#7188=EDGE_CURVE('',#5589,#5590,#4270,.T.);
#7189=EDGE_CURVE('',#5590,#5591,#4271,.T.);
#7190=EDGE_CURVE('',#5591,#5592,#4272,.T.);
#7191=EDGE_CURVE('',#5592,#5593,#683,.T.);
#7192=EDGE_CURVE('',#5594,#5593,#4273,.T.);
#7193=EDGE_CURVE('',#5594,#5595,#684,.T.);
#7194=EDGE_CURVE('',#5595,#5591,#4274,.T.);
#7195=EDGE_CURVE('',#5590,#5596,#4275,.T.);
#7196=EDGE_CURVE('',#5596,#5597,#685,.T.);
#7197=EDGE_CURVE('',#5598,#5597,#4276,.T.);
#7198=EDGE_CURVE('',#5598,#5589,#686,.T.);
#7199=EDGE_CURVE('',#5599,#5599,#4277,.T.);
#7200=EDGE_CURVE('',#5600,#5600,#4278,.T.);
#7201=EDGE_CURVE('',#5601,#5601,#4279,.T.);
#7202=EDGE_CURVE('',#5601,#5602,#4280,.T.);
#7203=EDGE_CURVE('',#5602,#5602,#4281,.T.);
#7204=EDGE_CURVE('',#5603,#5604,#687,.T.);
#7205=EDGE_CURVE('',#5603,#5605,#688,.T.);
#7206=EDGE_CURVE('',#5605,#5606,#689,.T.);
#7207=EDGE_CURVE('',#5606,#5604,#690,.T.);
#7208=EDGE_CURVE('',#5607,#5608,#691,.T.);
#7209=EDGE_CURVE('',#5607,#5609,#692,.T.);
#7210=EDGE_CURVE('',#5609,#5610,#693,.T.);
#7211=EDGE_CURVE('',#5610,#5608,#694,.T.);
#7212=EDGE_CURVE('',#5610,#5572,#4282,.T.);
#7213=EDGE_CURVE('',#5608,#5571,#4283,.T.);
#7214=EDGE_CURVE('',#5569,#5607,#4284,.T.);
#7215=EDGE_CURVE('',#5570,#5609,#4285,.T.);
#7216=EDGE_CURVE('',#5597,#5594,#4286,.T.);
#7217=EDGE_CURVE('',#5593,#5598,#4287,.T.);
#7218=EDGE_CURVE('',#5596,#5595,#4288,.T.);
#7219=EDGE_CURVE('',#5592,#5589,#4289,.T.);
#7220=EDGE_CURVE('',#5576,#5549,#4290,.T.);
#7221=EDGE_CURVE('',#5550,#5575,#4291,.T.);
#7222=EDGE_CURVE('',#5574,#5547,#4292,.T.);
#7223=EDGE_CURVE('',#5548,#5573,#4293,.T.);
#7224=EDGE_CURVE('',#5563,#5560,#4294,.T.);
#7225=EDGE_CURVE('',#5562,#5561,#4295,.T.);
#7226=EDGE_CURVE('',#5558,#5555,#4296,.T.);
#7227=EDGE_CURVE('',#5559,#5564,#4297,.T.);
#7228=EDGE_CURVE('',#5554,#5527,#4298,.T.);
#7229=EDGE_CURVE('',#5528,#5553,#4299,.T.);
#7230=EDGE_CURVE('',#5552,#5525,#4300,.T.);
#7231=EDGE_CURVE('',#5526,#5551,#4301,.T.);
#7232=EDGE_CURVE('',#5541,#5538,#4302,.T.);
#7233=EDGE_CURVE('',#5540,#5539,#4303,.T.);
#7234=EDGE_CURVE('',#5536,#5533,#4304,.T.);
#7235=EDGE_CURVE('',#5537,#5542,#4305,.T.);
#7236=EDGE_CURVE('',#5532,#5505,#4306,.T.);
#7237=EDGE_CURVE('',#5506,#5531,#4307,.T.);
#7238=EDGE_CURVE('',#5530,#5503,#4308,.T.);
#7239=EDGE_CURVE('',#5504,#5529,#4309,.T.);
#7240=EDGE_CURVE('',#5519,#5516,#4310,.T.);
#7241=EDGE_CURVE('',#5518,#5517,#4311,.T.);
#7242=EDGE_CURVE('',#5514,#5511,#4312,.T.);
#7243=EDGE_CURVE('',#5515,#5520,#4313,.T.);
#7244=EDGE_CURVE('',#5510,#5483,#4314,.T.);
#7245=EDGE_CURVE('',#5484,#5509,#4315,.T.);
#7246=EDGE_CURVE('',#5508,#5481,#4316,.T.);
#7247=EDGE_CURVE('',#5482,#5507,#4317,.T.);
#7248=EDGE_CURVE('',#5497,#5494,#4318,.T.);
#7249=EDGE_CURVE('',#5496,#5495,#4319,.T.);
#7250=EDGE_CURVE('',#5492,#5489,#4320,.T.);
#7251=EDGE_CURVE('',#5493,#5498,#4321,.T.);
#7252=EDGE_CURVE('',#5488,#5461,#4322,.T.);
#7253=EDGE_CURVE('',#5462,#5487,#4323,.T.);
#7254=EDGE_CURVE('',#5486,#5459,#4324,.T.);
#7255=EDGE_CURVE('',#5460,#5485,#4325,.T.);
#7256=EDGE_CURVE('',#5475,#5472,#4326,.T.);
#7257=EDGE_CURVE('',#5474,#5473,#4327,.T.);
#7258=EDGE_CURVE('',#5470,#5467,#4328,.T.);
#7259=EDGE_CURVE('',#5471,#5476,#4329,.T.);
#7260=EDGE_CURVE('',#5466,#5605,#4330,.T.);
#7261=EDGE_CURVE('',#5606,#5465,#4331,.T.);
#7262=EDGE_CURVE('',#5464,#5603,#4332,.T.);
#7263=EDGE_CURVE('',#5604,#5463,#4333,.T.);
#7264=EDGE_CURVE('',#5579,#5585,#4334,.T.);
#7265=EDGE_CURVE('',#5584,#5580,#4335,.T.);
#7266=EDGE_CURVE('',#5577,#5586,#4336,.T.);
#7267=EDGE_CURVE('',#5583,#5581,#4337,.T.);
#9635=ORIENTED_EDGE('',*,*,#6979,.F.);
#9636=ORIENTED_EDGE('',*,*,#6980,.T.);
#9637=ORIENTED_EDGE('',*,*,#6981,.T.);
#9638=ORIENTED_EDGE('',*,*,#6980,.F.);
#9639=ORIENTED_EDGE('',*,*,#6982,.F.);
#9640=ORIENTED_EDGE('',*,*,#6983,.F.);
#9641=ORIENTED_EDGE('',*,*,#6984,.T.);
#9642=ORIENTED_EDGE('',*,*,#6985,.F.);
#9643=ORIENTED_EDGE('',*,*,#6986,.F.);
#9644=ORIENTED_EDGE('',*,*,#6984,.F.);
#9645=ORIENTED_EDGE('',*,*,#6987,.F.);
#9646=ORIENTED_EDGE('',*,*,#6988,.F.);
#9647=ORIENTED_EDGE('',*,*,#6989,.T.);
#9648=ORIENTED_EDGE('',*,*,#6990,.F.);
#9649=ORIENTED_EDGE('',*,*,#6989,.F.);
#9650=ORIENTED_EDGE('',*,*,#6982,.T.);
#9651=ORIENTED_EDGE('',*,*,#6983,.T.);
#9652=ORIENTED_EDGE('',*,*,#6991,.T.);
#9653=ORIENTED_EDGE('',*,*,#6992,.T.);
#9654=ORIENTED_EDGE('',*,*,#6991,.F.);
#9655=ORIENTED_EDGE('',*,*,#6987,.T.);
#9656=ORIENTED_EDGE('',*,*,#6988,.T.);
#9657=ORIENTED_EDGE('',*,*,#6993,.T.);
#9658=ORIENTED_EDGE('',*,*,#6985,.T.);
#9659=ORIENTED_EDGE('',*,*,#6986,.T.);
#9660=ORIENTED_EDGE('',*,*,#6993,.F.);
#9661=ORIENTED_EDGE('',*,*,#6990,.T.);
#9662=ORIENTED_EDGE('',*,*,#6994,.T.);
#9663=ORIENTED_EDGE('',*,*,#6995,.F.);
#9664=ORIENTED_EDGE('',*,*,#6994,.F.);
#9665=ORIENTED_EDGE('',*,*,#6981,.F.);
#9666=ORIENTED_EDGE('',*,*,#6996,.T.);
#9667=ORIENTED_EDGE('',*,*,#6997,.T.);
#9668=ORIENTED_EDGE('',*,*,#6996,.F.);
#9669=ORIENTED_EDGE('',*,*,#6998,.F.);
#9670=ORIENTED_EDGE('',*,*,#6999,.T.);
#9671=ORIENTED_EDGE('',*,*,#6979,.T.);
#9672=ORIENTED_EDGE('',*,*,#6999,.F.);
#9673=ORIENTED_EDGE('',*,*,#6998,.T.);
#9674=ORIENTED_EDGE('',*,*,#6992,.F.);
#9675=ORIENTED_EDGE('',*,*,#6997,.F.);
#9676=ORIENTED_EDGE('',*,*,#6995,.T.);
#9677=ORIENTED_EDGE('',*,*,#7000,.T.);
#9678=ORIENTED_EDGE('',*,*,#7000,.F.);
#9679=ORIENTED_EDGE('',*,*,#7001,.T.);
#9680=ORIENTED_EDGE('',*,*,#7001,.F.);
#9681=ORIENTED_EDGE('',*,*,#7002,.T.);
#9682=ORIENTED_EDGE('',*,*,#7002,.F.);
#9683=ORIENTED_EDGE('',*,*,#7003,.T.);
#9684=ORIENTED_EDGE('',*,*,#7003,.F.);
#9685=ORIENTED_EDGE('',*,*,#7004,.T.);
#9686=ORIENTED_EDGE('',*,*,#7004,.F.);
#9687=ORIENTED_EDGE('',*,*,#7005,.T.);
#9688=ORIENTED_EDGE('',*,*,#7005,.F.);
#9689=ORIENTED_EDGE('',*,*,#7006,.T.);
#9690=ORIENTED_EDGE('',*,*,#7006,.F.);
#9691=ORIENTED_EDGE('',*,*,#7007,.F.);
#9692=ORIENTED_EDGE('',*,*,#7008,.T.);
#9693=ORIENTED_EDGE('',*,*,#7009,.F.);
#9694=ORIENTED_EDGE('',*,*,#7010,.F.);
#9695=ORIENTED_EDGE('',*,*,#7008,.F.);
#9696=ORIENTED_EDGE('',*,*,#7011,.F.);
#9697=ORIENTED_EDGE('',*,*,#7012,.T.);
#9698=ORIENTED_EDGE('',*,*,#7013,.F.);
#9699=ORIENTED_EDGE('',*,*,#7012,.F.);
#9700=ORIENTED_EDGE('',*,*,#7014,.F.);
#9701=ORIENTED_EDGE('',*,*,#7015,.T.);
#9702=ORIENTED_EDGE('',*,*,#7016,.F.);
#9703=ORIENTED_EDGE('',*,*,#7015,.F.);
#9704=ORIENTED_EDGE('',*,*,#7017,.F.);
#9705=ORIENTED_EDGE('',*,*,#7018,.F.);
#9706=ORIENTED_EDGE('',*,*,#7019,.T.);
#9707=ORIENTED_EDGE('',*,*,#7020,.F.);
#9708=ORIENTED_EDGE('',*,*,#7019,.F.);
#9709=ORIENTED_EDGE('',*,*,#7021,.F.);
#9710=ORIENTED_EDGE('',*,*,#7022,.T.);
#9711=ORIENTED_EDGE('',*,*,#7023,.T.);
#9712=ORIENTED_EDGE('',*,*,#7022,.F.);
#9713=ORIENTED_EDGE('',*,*,#7024,.F.);
#9714=ORIENTED_EDGE('',*,*,#7025,.T.);
#9715=ORIENTED_EDGE('',*,*,#7009,.T.);
#9716=ORIENTED_EDGE('',*,*,#7010,.T.);
#9717=ORIENTED_EDGE('',*,*,#7025,.F.);
#9718=ORIENTED_EDGE('',*,*,#7017,.T.);
#9719=ORIENTED_EDGE('',*,*,#7018,.T.);
#9720=ORIENTED_EDGE('',*,*,#7026,.T.);
#9721=ORIENTED_EDGE('',*,*,#7027,.T.);
#9722=ORIENTED_EDGE('',*,*,#7026,.F.);
#9723=ORIENTED_EDGE('',*,*,#7027,.F.);
#9724=ORIENTED_EDGE('',*,*,#7028,.T.);
#9725=ORIENTED_EDGE('',*,*,#7029,.T.);
#9726=ORIENTED_EDGE('',*,*,#7028,.F.);
#9727=ORIENTED_EDGE('',*,*,#7029,.F.);
#9728=ORIENTED_EDGE('',*,*,#7030,.T.);
#9729=ORIENTED_EDGE('',*,*,#7011,.T.);
#9730=ORIENTED_EDGE('',*,*,#7030,.F.);
#9731=ORIENTED_EDGE('',*,*,#7016,.T.);
#9732=ORIENTED_EDGE('',*,*,#7031,.T.);
#9733=ORIENTED_EDGE('',*,*,#7032,.T.);
#9734=ORIENTED_EDGE('',*,*,#7031,.F.);
#9735=ORIENTED_EDGE('',*,*,#7033,.F.);
#9736=ORIENTED_EDGE('',*,*,#7034,.T.);
#9737=ORIENTED_EDGE('',*,*,#7035,.T.);
#9738=ORIENTED_EDGE('',*,*,#7034,.F.);
#9739=ORIENTED_EDGE('',*,*,#7036,.F.);
#9740=ORIENTED_EDGE('',*,*,#7037,.T.);
#9741=ORIENTED_EDGE('',*,*,#7038,.T.);
#9742=ORIENTED_EDGE('',*,*,#7037,.F.);
#9743=ORIENTED_EDGE('',*,*,#7039,.T.);
#9744=ORIENTED_EDGE('',*,*,#7040,.T.);
#9745=ORIENTED_EDGE('',*,*,#7041,.F.);
#9746=ORIENTED_EDGE('',*,*,#7040,.F.);
#9747=ORIENTED_EDGE('',*,*,#7042,.T.);
#9748=ORIENTED_EDGE('',*,*,#7039,.F.);
#9749=ORIENTED_EDGE('',*,*,#7043,.T.);
#9750=ORIENTED_EDGE('',*,*,#7036,.T.);
#9751=ORIENTED_EDGE('',*,*,#7043,.F.);
#9752=ORIENTED_EDGE('',*,*,#7042,.F.);
#9753=ORIENTED_EDGE('',*,*,#7041,.T.);
#9754=ORIENTED_EDGE('',*,*,#7007,.T.);
#9755=ORIENTED_EDGE('',*,*,#7038,.F.);
#9756=ORIENTED_EDGE('',*,*,#7014,.T.);
#9757=ORIENTED_EDGE('',*,*,#7035,.F.);
#9758=ORIENTED_EDGE('',*,*,#7020,.T.);
#9759=ORIENTED_EDGE('',*,*,#7033,.T.);
#9760=ORIENTED_EDGE('',*,*,#7032,.F.);
#9761=ORIENTED_EDGE('',*,*,#7023,.F.);
#9762=ORIENTED_EDGE('',*,*,#7024,.T.);
#9763=ORIENTED_EDGE('',*,*,#7021,.T.);
#9764=ORIENTED_EDGE('',*,*,#7013,.T.);
#9765=ORIENTED_EDGE('',*,*,#7044,.F.);
#9766=ORIENTED_EDGE('',*,*,#7045,.T.);
#9767=ORIENTED_EDGE('',*,*,#7046,.T.);
#9768=ORIENTED_EDGE('',*,*,#7045,.F.);
#9769=ORIENTED_EDGE('',*,*,#7047,.F.);
#9770=ORIENTED_EDGE('',*,*,#7048,.T.);
#9771=ORIENTED_EDGE('',*,*,#7049,.T.);
#9772=ORIENTED_EDGE('',*,*,#7050,.T.);
#9773=ORIENTED_EDGE('',*,*,#7051,.F.);
#9774=ORIENTED_EDGE('',*,*,#7052,.T.);
#9775=ORIENTED_EDGE('',*,*,#7053,.T.);
#9776=ORIENTED_EDGE('',*,*,#7054,.T.);
#9777=ORIENTED_EDGE('',*,*,#7055,.T.);
#9778=ORIENTED_EDGE('',*,*,#7056,.T.);
#9779=ORIENTED_EDGE('',*,*,#7057,.T.);
#9780=ORIENTED_EDGE('',*,*,#7058,.T.);
#9781=ORIENTED_EDGE('',*,*,#7059,.F.);
#9782=ORIENTED_EDGE('',*,*,#7060,.T.);
#9783=ORIENTED_EDGE('',*,*,#7061,.T.);
#9784=ORIENTED_EDGE('',*,*,#7056,.F.);
#9785=ORIENTED_EDGE('',*,*,#7062,.T.);
#9786=ORIENTED_EDGE('',*,*,#7063,.T.);
#9787=ORIENTED_EDGE('',*,*,#7064,.F.);
#9788=ORIENTED_EDGE('',*,*,#7065,.T.);
#9789=ORIENTED_EDGE('',*,*,#7066,.F.);
#9790=ORIENTED_EDGE('',*,*,#7067,.T.);
#9791=ORIENTED_EDGE('',*,*,#7068,.F.);
#9792=ORIENTED_EDGE('',*,*,#7069,.T.);
#9793=ORIENTED_EDGE('',*,*,#7070,.T.);
#9794=ORIENTED_EDGE('',*,*,#7069,.F.);
#9795=ORIENTED_EDGE('',*,*,#7071,.F.);
#9796=ORIENTED_EDGE('',*,*,#7072,.T.);
#9797=ORIENTED_EDGE('',*,*,#7073,.T.);
#9798=ORIENTED_EDGE('',*,*,#7074,.T.);
#9799=ORIENTED_EDGE('',*,*,#7075,.F.);
#9800=ORIENTED_EDGE('',*,*,#7076,.T.);
#9801=ORIENTED_EDGE('',*,*,#7077,.T.);
#9802=ORIENTED_EDGE('',*,*,#7078,.T.);
#9803=ORIENTED_EDGE('',*,*,#7079,.T.);
#9804=ORIENTED_EDGE('',*,*,#7080,.T.);
#9805=ORIENTED_EDGE('',*,*,#7081,.T.);
#9806=ORIENTED_EDGE('',*,*,#7082,.T.);
#9807=ORIENTED_EDGE('',*,*,#7083,.F.);
#9808=ORIENTED_EDGE('',*,*,#7084,.T.);
#9809=ORIENTED_EDGE('',*,*,#7085,.T.);
#9810=ORIENTED_EDGE('',*,*,#7080,.F.);
#9811=ORIENTED_EDGE('',*,*,#7086,.T.);
#9812=ORIENTED_EDGE('',*,*,#7087,.T.);
#9813=ORIENTED_EDGE('',*,*,#7088,.F.);
#9814=ORIENTED_EDGE('',*,*,#7089,.T.);
#9815=ORIENTED_EDGE('',*,*,#7090,.F.);
#9816=ORIENTED_EDGE('',*,*,#7091,.T.);
#9817=ORIENTED_EDGE('',*,*,#7092,.F.);
#9818=ORIENTED_EDGE('',*,*,#7093,.T.);
#9819=ORIENTED_EDGE('',*,*,#7094,.T.);
#9820=ORIENTED_EDGE('',*,*,#7093,.F.);
#9821=ORIENTED_EDGE('',*,*,#7095,.F.);
#9822=ORIENTED_EDGE('',*,*,#7096,.T.);
#9823=ORIENTED_EDGE('',*,*,#7097,.T.);
#9824=ORIENTED_EDGE('',*,*,#7098,.T.);
#9825=ORIENTED_EDGE('',*,*,#7099,.F.);
#9826=ORIENTED_EDGE('',*,*,#7100,.T.);
#9827=ORIENTED_EDGE('',*,*,#7101,.T.);
#9828=ORIENTED_EDGE('',*,*,#7102,.T.);
#9829=ORIENTED_EDGE('',*,*,#7103,.T.);
#9830=ORIENTED_EDGE('',*,*,#7104,.T.);
#9831=ORIENTED_EDGE('',*,*,#7105,.T.);
#9832=ORIENTED_EDGE('',*,*,#7106,.T.);
#9833=ORIENTED_EDGE('',*,*,#7107,.F.);
#9834=ORIENTED_EDGE('',*,*,#7108,.T.);
#9835=ORIENTED_EDGE('',*,*,#7109,.T.);
#9836=ORIENTED_EDGE('',*,*,#7104,.F.);
#9837=ORIENTED_EDGE('',*,*,#7110,.T.);
#9838=ORIENTED_EDGE('',*,*,#7111,.T.);
#9839=ORIENTED_EDGE('',*,*,#7112,.F.);
#9840=ORIENTED_EDGE('',*,*,#7113,.T.);
#9841=ORIENTED_EDGE('',*,*,#7114,.F.);
#9842=ORIENTED_EDGE('',*,*,#7115,.T.);
#9843=ORIENTED_EDGE('',*,*,#7116,.F.);
#9844=ORIENTED_EDGE('',*,*,#7117,.T.);
#9845=ORIENTED_EDGE('',*,*,#7118,.T.);
#9846=ORIENTED_EDGE('',*,*,#7117,.F.);
#9847=ORIENTED_EDGE('',*,*,#7119,.F.);
#9848=ORIENTED_EDGE('',*,*,#7120,.T.);
#9849=ORIENTED_EDGE('',*,*,#7121,.T.);
#9850=ORIENTED_EDGE('',*,*,#7122,.T.);
#9851=ORIENTED_EDGE('',*,*,#7123,.F.);
#9852=ORIENTED_EDGE('',*,*,#7124,.T.);
#9853=ORIENTED_EDGE('',*,*,#7125,.T.);
#9854=ORIENTED_EDGE('',*,*,#7126,.T.);
#9855=ORIENTED_EDGE('',*,*,#7127,.T.);
#9856=ORIENTED_EDGE('',*,*,#7128,.T.);
#9857=ORIENTED_EDGE('',*,*,#7129,.T.);
#9858=ORIENTED_EDGE('',*,*,#7130,.T.);
#9859=ORIENTED_EDGE('',*,*,#7131,.F.);
#9860=ORIENTED_EDGE('',*,*,#7132,.T.);
#9861=ORIENTED_EDGE('',*,*,#7133,.T.);
#9862=ORIENTED_EDGE('',*,*,#7128,.F.);
#9863=ORIENTED_EDGE('',*,*,#7134,.T.);
#9864=ORIENTED_EDGE('',*,*,#7135,.T.);
#9865=ORIENTED_EDGE('',*,*,#7136,.F.);
#9866=ORIENTED_EDGE('',*,*,#7137,.T.);
#9867=ORIENTED_EDGE('',*,*,#7138,.F.);
#9868=ORIENTED_EDGE('',*,*,#7139,.T.);
#9869=ORIENTED_EDGE('',*,*,#7140,.F.);
#9870=ORIENTED_EDGE('',*,*,#7141,.T.);
#9871=ORIENTED_EDGE('',*,*,#7142,.T.);
#9872=ORIENTED_EDGE('',*,*,#7141,.F.);
#9873=ORIENTED_EDGE('',*,*,#7143,.F.);
#9874=ORIENTED_EDGE('',*,*,#7144,.T.);
#9875=ORIENTED_EDGE('',*,*,#7145,.T.);
#9876=ORIENTED_EDGE('',*,*,#7146,.T.);
#9877=ORIENTED_EDGE('',*,*,#7147,.F.);
#9878=ORIENTED_EDGE('',*,*,#7148,.T.);
#9879=ORIENTED_EDGE('',*,*,#7149,.T.);
#9880=ORIENTED_EDGE('',*,*,#7150,.T.);
#9881=ORIENTED_EDGE('',*,*,#7151,.T.);
#9882=ORIENTED_EDGE('',*,*,#7152,.T.);
#9883=ORIENTED_EDGE('',*,*,#7153,.T.);
#9884=ORIENTED_EDGE('',*,*,#7154,.T.);
#9885=ORIENTED_EDGE('',*,*,#7155,.F.);
#9886=ORIENTED_EDGE('',*,*,#7156,.T.);
#9887=ORIENTED_EDGE('',*,*,#7157,.T.);
#9888=ORIENTED_EDGE('',*,*,#7152,.F.);
#9889=ORIENTED_EDGE('',*,*,#7158,.T.);
#9890=ORIENTED_EDGE('',*,*,#7159,.T.);
#9891=ORIENTED_EDGE('',*,*,#7160,.F.);
#9892=ORIENTED_EDGE('',*,*,#7161,.T.);
#9893=ORIENTED_EDGE('',*,*,#7162,.F.);
#9894=ORIENTED_EDGE('',*,*,#7163,.T.);
#9895=ORIENTED_EDGE('',*,*,#7164,.F.);
#9896=ORIENTED_EDGE('',*,*,#7165,.T.);
#9897=ORIENTED_EDGE('',*,*,#7166,.T.);
#9898=ORIENTED_EDGE('',*,*,#7165,.F.);
#9899=ORIENTED_EDGE('',*,*,#7167,.F.);
#9900=ORIENTED_EDGE('',*,*,#7168,.T.);
#9901=ORIENTED_EDGE('',*,*,#7169,.F.);
#9902=ORIENTED_EDGE('',*,*,#7170,.F.);
#9903=ORIENTED_EDGE('',*,*,#7171,.F.);
#9904=ORIENTED_EDGE('',*,*,#7172,.T.);
#9905=ORIENTED_EDGE('',*,*,#7173,.T.);
#9906=ORIENTED_EDGE('',*,*,#7174,.T.);
#9907=ORIENTED_EDGE('',*,*,#7175,.F.);
#9908=ORIENTED_EDGE('',*,*,#7176,.F.);
#9909=ORIENTED_EDGE('',*,*,#7177,.T.);
#9910=ORIENTED_EDGE('',*,*,#7178,.F.);
#9911=ORIENTED_EDGE('',*,*,#7179,.F.);
#9912=ORIENTED_EDGE('',*,*,#7180,.T.);
#9913=ORIENTED_EDGE('',*,*,#7181,.T.);
#9914=ORIENTED_EDGE('',*,*,#7182,.T.);
#9915=ORIENTED_EDGE('',*,*,#7183,.F.);
#9916=ORIENTED_EDGE('',*,*,#7184,.T.);
#9917=ORIENTED_EDGE('',*,*,#7185,.T.);
#9918=ORIENTED_EDGE('',*,*,#7180,.F.);
#9919=ORIENTED_EDGE('',*,*,#7186,.F.);
#9920=ORIENTED_EDGE('',*,*,#7187,.T.);
#9921=ORIENTED_EDGE('',*,*,#7188,.T.);
#9922=ORIENTED_EDGE('',*,*,#7189,.T.);
#9923=ORIENTED_EDGE('',*,*,#7190,.T.);
#9924=ORIENTED_EDGE('',*,*,#7191,.T.);
#9925=ORIENTED_EDGE('',*,*,#7192,.F.);
#9926=ORIENTED_EDGE('',*,*,#7193,.T.);
#9927=ORIENTED_EDGE('',*,*,#7194,.T.);
#9928=ORIENTED_EDGE('',*,*,#7189,.F.);
#9929=ORIENTED_EDGE('',*,*,#7195,.T.);
#9930=ORIENTED_EDGE('',*,*,#7196,.T.);
#9931=ORIENTED_EDGE('',*,*,#7197,.F.);
#9932=ORIENTED_EDGE('',*,*,#7198,.T.);
#9933=ORIENTED_EDGE('',*,*,#7199,.F.);
#9934=ORIENTED_EDGE('',*,*,#7200,.T.);
#9935=ORIENTED_EDGE('',*,*,#7201,.F.);
#9936=ORIENTED_EDGE('',*,*,#7202,.T.);
#9937=ORIENTED_EDGE('',*,*,#7203,.T.);
#9938=ORIENTED_EDGE('',*,*,#7202,.F.);
#9939=ORIENTED_EDGE('',*,*,#7204,.F.);
#9940=ORIENTED_EDGE('',*,*,#7205,.T.);
#9941=ORIENTED_EDGE('',*,*,#7206,.T.);
#9942=ORIENTED_EDGE('',*,*,#7207,.T.);
#9943=ORIENTED_EDGE('',*,*,#7208,.F.);
#9944=ORIENTED_EDGE('',*,*,#7209,.T.);
#9945=ORIENTED_EDGE('',*,*,#7210,.T.);
#9946=ORIENTED_EDGE('',*,*,#7211,.T.);
#9947=ORIENTED_EDGE('',*,*,#7212,.T.);
#9948=ORIENTED_EDGE('',*,*,#7169,.T.);
#9949=ORIENTED_EDGE('',*,*,#7213,.F.);
#9950=ORIENTED_EDGE('',*,*,#7211,.F.);
#9951=ORIENTED_EDGE('',*,*,#7214,.F.);
#9952=ORIENTED_EDGE('',*,*,#7167,.T.);
#9953=ORIENTED_EDGE('',*,*,#7215,.T.);
#9954=ORIENTED_EDGE('',*,*,#7209,.F.);
#9955=ORIENTED_EDGE('',*,*,#7168,.F.);
#9956=ORIENTED_EDGE('',*,*,#7214,.T.);
#9957=ORIENTED_EDGE('',*,*,#7208,.T.);
#9958=ORIENTED_EDGE('',*,*,#7213,.T.);
#9959=ORIENTED_EDGE('',*,*,#7215,.F.);
#9960=ORIENTED_EDGE('',*,*,#7170,.T.);
#9961=ORIENTED_EDGE('',*,*,#7212,.F.);
#9962=ORIENTED_EDGE('',*,*,#7210,.F.);
#9963=ORIENTED_EDGE('',*,*,#7201,.T.);
#9964=ORIENTED_EDGE('',*,*,#7200,.F.);
#9965=ORIENTED_EDGE('',*,*,#7203,.F.);
#9966=ORIENTED_EDGE('',*,*,#7199,.T.);
#9967=ORIENTED_EDGE('',*,*,#7216,.T.);
#9968=ORIENTED_EDGE('',*,*,#7192,.T.);
#9969=ORIENTED_EDGE('',*,*,#7217,.T.);
#9970=ORIENTED_EDGE('',*,*,#7197,.T.);
#9971=ORIENTED_EDGE('',*,*,#7194,.F.);
#9972=ORIENTED_EDGE('',*,*,#7218,.F.);
#9973=ORIENTED_EDGE('',*,*,#7195,.F.);
#9974=ORIENTED_EDGE('',*,*,#7188,.F.);
#9975=ORIENTED_EDGE('',*,*,#7219,.F.);
#9976=ORIENTED_EDGE('',*,*,#7190,.F.);
#9977=ORIENTED_EDGE('',*,*,#7191,.F.);
#9978=ORIENTED_EDGE('',*,*,#7219,.T.);
#9979=ORIENTED_EDGE('',*,*,#7198,.F.);
#9980=ORIENTED_EDGE('',*,*,#7217,.F.);
#9981=ORIENTED_EDGE('',*,*,#7193,.F.);
#9982=ORIENTED_EDGE('',*,*,#7216,.F.);
#9983=ORIENTED_EDGE('',*,*,#7196,.F.);
#9984=ORIENTED_EDGE('',*,*,#7218,.T.);
#9985=ORIENTED_EDGE('',*,*,#7166,.F.);
#9986=ORIENTED_EDGE('',*,*,#7186,.T.);
#9987=ORIENTED_EDGE('',*,*,#7164,.T.);
#9988=ORIENTED_EDGE('',*,*,#7187,.F.);
#9989=ORIENTED_EDGE('',*,*,#7145,.F.);
#9990=ORIENTED_EDGE('',*,*,#7220,.F.);
#9991=ORIENTED_EDGE('',*,*,#7173,.F.);
#9992=ORIENTED_EDGE('',*,*,#7221,.F.);
#9993=ORIENTED_EDGE('',*,*,#7222,.T.);
#9994=ORIENTED_EDGE('',*,*,#7143,.T.);
#9995=ORIENTED_EDGE('',*,*,#7223,.T.);
#9996=ORIENTED_EDGE('',*,*,#7171,.T.);
#9997=ORIENTED_EDGE('',*,*,#7146,.F.);
#9998=ORIENTED_EDGE('',*,*,#7221,.T.);
#9999=ORIENTED_EDGE('',*,*,#7172,.F.);
#10000=ORIENTED_EDGE('',*,*,#7223,.F.);
#10001=ORIENTED_EDGE('',*,*,#7144,.F.);
#10002=ORIENTED_EDGE('',*,*,#7222,.F.);
#10003=ORIENTED_EDGE('',*,*,#7174,.F.);
#10004=ORIENTED_EDGE('',*,*,#7220,.T.);
#10005=ORIENTED_EDGE('',*,*,#7156,.F.);
#10006=ORIENTED_EDGE('',*,*,#7224,.F.);
#10007=ORIENTED_EDGE('',*,*,#7159,.F.);
#10008=ORIENTED_EDGE('',*,*,#7225,.T.);
#10009=ORIENTED_EDGE('',*,*,#7154,.F.);
#10010=ORIENTED_EDGE('',*,*,#7226,.T.);
#10011=ORIENTED_EDGE('',*,*,#7161,.F.);
#10012=ORIENTED_EDGE('',*,*,#7227,.F.);
#10013=ORIENTED_EDGE('',*,*,#7157,.F.);
#10014=ORIENTED_EDGE('',*,*,#7225,.F.);
#10015=ORIENTED_EDGE('',*,*,#7158,.F.);
#10016=ORIENTED_EDGE('',*,*,#7151,.F.);
#10017=ORIENTED_EDGE('',*,*,#7226,.F.);
#10018=ORIENTED_EDGE('',*,*,#7153,.F.);
#10019=ORIENTED_EDGE('',*,*,#7224,.T.);
#10020=ORIENTED_EDGE('',*,*,#7155,.T.);
#10021=ORIENTED_EDGE('',*,*,#7227,.T.);
#10022=ORIENTED_EDGE('',*,*,#7160,.T.);
#10023=ORIENTED_EDGE('',*,*,#7142,.F.);
#10024=ORIENTED_EDGE('',*,*,#7162,.T.);
#10025=ORIENTED_EDGE('',*,*,#7140,.T.);
#10026=ORIENTED_EDGE('',*,*,#7163,.F.);
#10027=ORIENTED_EDGE('',*,*,#7121,.F.);
#10028=ORIENTED_EDGE('',*,*,#7228,.F.);
#10029=ORIENTED_EDGE('',*,*,#7149,.F.);
#10030=ORIENTED_EDGE('',*,*,#7229,.F.);
#10031=ORIENTED_EDGE('',*,*,#7230,.T.);
#10032=ORIENTED_EDGE('',*,*,#7119,.T.);
#10033=ORIENTED_EDGE('',*,*,#7231,.T.);
#10034=ORIENTED_EDGE('',*,*,#7147,.T.);
#10035=ORIENTED_EDGE('',*,*,#7122,.F.);
#10036=ORIENTED_EDGE('',*,*,#7229,.T.);
#10037=ORIENTED_EDGE('',*,*,#7148,.F.);
#10038=ORIENTED_EDGE('',*,*,#7231,.F.);
#10039=ORIENTED_EDGE('',*,*,#7120,.F.);
#10040=ORIENTED_EDGE('',*,*,#7230,.F.);
#10041=ORIENTED_EDGE('',*,*,#7150,.F.);
#10042=ORIENTED_EDGE('',*,*,#7228,.T.);
#10043=ORIENTED_EDGE('',*,*,#7132,.F.);
#10044=ORIENTED_EDGE('',*,*,#7232,.F.);
#10045=ORIENTED_EDGE('',*,*,#7135,.F.);
#10046=ORIENTED_EDGE('',*,*,#7233,.T.);
#10047=ORIENTED_EDGE('',*,*,#7130,.F.);
#10048=ORIENTED_EDGE('',*,*,#7234,.T.);
#10049=ORIENTED_EDGE('',*,*,#7137,.F.);
#10050=ORIENTED_EDGE('',*,*,#7235,.F.);
#10051=ORIENTED_EDGE('',*,*,#7133,.F.);
#10052=ORIENTED_EDGE('',*,*,#7233,.F.);
#10053=ORIENTED_EDGE('',*,*,#7134,.F.);
#10054=ORIENTED_EDGE('',*,*,#7127,.F.);
#10055=ORIENTED_EDGE('',*,*,#7234,.F.);
#10056=ORIENTED_EDGE('',*,*,#7129,.F.);
#10057=ORIENTED_EDGE('',*,*,#7232,.T.);
#10058=ORIENTED_EDGE('',*,*,#7131,.T.);
#10059=ORIENTED_EDGE('',*,*,#7235,.T.);
#10060=ORIENTED_EDGE('',*,*,#7136,.T.);
#10061=ORIENTED_EDGE('',*,*,#7118,.F.);
#10062=ORIENTED_EDGE('',*,*,#7138,.T.);
#10063=ORIENTED_EDGE('',*,*,#7116,.T.);
#10064=ORIENTED_EDGE('',*,*,#7139,.F.);
#10065=ORIENTED_EDGE('',*,*,#7097,.F.);
#10066=ORIENTED_EDGE('',*,*,#7236,.F.);
#10067=ORIENTED_EDGE('',*,*,#7125,.F.);
#10068=ORIENTED_EDGE('',*,*,#7237,.F.);
#10069=ORIENTED_EDGE('',*,*,#7238,.T.);
#10070=ORIENTED_EDGE('',*,*,#7095,.T.);
#10071=ORIENTED_EDGE('',*,*,#7239,.T.);
#10072=ORIENTED_EDGE('',*,*,#7123,.T.);
#10073=ORIENTED_EDGE('',*,*,#7098,.F.);
#10074=ORIENTED_EDGE('',*,*,#7237,.T.);
#10075=ORIENTED_EDGE('',*,*,#7124,.F.);
#10076=ORIENTED_EDGE('',*,*,#7239,.F.);
#10077=ORIENTED_EDGE('',*,*,#7096,.F.);
#10078=ORIENTED_EDGE('',*,*,#7238,.F.);
#10079=ORIENTED_EDGE('',*,*,#7126,.F.);
#10080=ORIENTED_EDGE('',*,*,#7236,.T.);
#10081=ORIENTED_EDGE('',*,*,#7108,.F.);
#10082=ORIENTED_EDGE('',*,*,#7240,.F.);
#10083=ORIENTED_EDGE('',*,*,#7111,.F.);
#10084=ORIENTED_EDGE('',*,*,#7241,.T.);
#10085=ORIENTED_EDGE('',*,*,#7106,.F.);
#10086=ORIENTED_EDGE('',*,*,#7242,.T.);
#10087=ORIENTED_EDGE('',*,*,#7113,.F.);
#10088=ORIENTED_EDGE('',*,*,#7243,.F.);
#10089=ORIENTED_EDGE('',*,*,#7109,.F.);
#10090=ORIENTED_EDGE('',*,*,#7241,.F.);
#10091=ORIENTED_EDGE('',*,*,#7110,.F.);
#10092=ORIENTED_EDGE('',*,*,#7103,.F.);
#10093=ORIENTED_EDGE('',*,*,#7242,.F.);
#10094=ORIENTED_EDGE('',*,*,#7105,.F.);
#10095=ORIENTED_EDGE('',*,*,#7240,.T.);
#10096=ORIENTED_EDGE('',*,*,#7107,.T.);
#10097=ORIENTED_EDGE('',*,*,#7243,.T.);
#10098=ORIENTED_EDGE('',*,*,#7112,.T.);
#10099=ORIENTED_EDGE('',*,*,#7094,.F.);
#10100=ORIENTED_EDGE('',*,*,#7114,.T.);
#10101=ORIENTED_EDGE('',*,*,#7092,.T.);
#10102=ORIENTED_EDGE('',*,*,#7115,.F.);
#10103=ORIENTED_EDGE('',*,*,#7073,.F.);
#10104=ORIENTED_EDGE('',*,*,#7244,.F.);
#10105=ORIENTED_EDGE('',*,*,#7101,.F.);
#10106=ORIENTED_EDGE('',*,*,#7245,.F.);
#10107=ORIENTED_EDGE('',*,*,#7246,.T.);
#10108=ORIENTED_EDGE('',*,*,#7071,.T.);
#10109=ORIENTED_EDGE('',*,*,#7247,.T.);
#10110=ORIENTED_EDGE('',*,*,#7099,.T.);
#10111=ORIENTED_EDGE('',*,*,#7074,.F.);
#10112=ORIENTED_EDGE('',*,*,#7245,.T.);
#10113=ORIENTED_EDGE('',*,*,#7100,.F.);
#10114=ORIENTED_EDGE('',*,*,#7247,.F.);
#10115=ORIENTED_EDGE('',*,*,#7072,.F.);
#10116=ORIENTED_EDGE('',*,*,#7246,.F.);
#10117=ORIENTED_EDGE('',*,*,#7102,.F.);
#10118=ORIENTED_EDGE('',*,*,#7244,.T.);
#10119=ORIENTED_EDGE('',*,*,#7084,.F.);
#10120=ORIENTED_EDGE('',*,*,#7248,.F.);
#10121=ORIENTED_EDGE('',*,*,#7087,.F.);
#10122=ORIENTED_EDGE('',*,*,#7249,.T.);
#10123=ORIENTED_EDGE('',*,*,#7082,.F.);
#10124=ORIENTED_EDGE('',*,*,#7250,.T.);
#10125=ORIENTED_EDGE('',*,*,#7089,.F.);
#10126=ORIENTED_EDGE('',*,*,#7251,.F.);
#10127=ORIENTED_EDGE('',*,*,#7085,.F.);
#10128=ORIENTED_EDGE('',*,*,#7249,.F.);
#10129=ORIENTED_EDGE('',*,*,#7086,.F.);
#10130=ORIENTED_EDGE('',*,*,#7079,.F.);
#10131=ORIENTED_EDGE('',*,*,#7250,.F.);
#10132=ORIENTED_EDGE('',*,*,#7081,.F.);
#10133=ORIENTED_EDGE('',*,*,#7248,.T.);
#10134=ORIENTED_EDGE('',*,*,#7083,.T.);
#10135=ORIENTED_EDGE('',*,*,#7251,.T.);
#10136=ORIENTED_EDGE('',*,*,#7088,.T.);
#10137=ORIENTED_EDGE('',*,*,#7070,.F.);
#10138=ORIENTED_EDGE('',*,*,#7090,.T.);
#10139=ORIENTED_EDGE('',*,*,#7068,.T.);
#10140=ORIENTED_EDGE('',*,*,#7091,.F.);
#10141=ORIENTED_EDGE('',*,*,#7049,.F.);
#10142=ORIENTED_EDGE('',*,*,#7252,.F.);
#10143=ORIENTED_EDGE('',*,*,#7077,.F.);
#10144=ORIENTED_EDGE('',*,*,#7253,.F.);
#10145=ORIENTED_EDGE('',*,*,#7254,.T.);
#10146=ORIENTED_EDGE('',*,*,#7047,.T.);
#10147=ORIENTED_EDGE('',*,*,#7255,.T.);
#10148=ORIENTED_EDGE('',*,*,#7075,.T.);
#10149=ORIENTED_EDGE('',*,*,#7050,.F.);
#10150=ORIENTED_EDGE('',*,*,#7253,.T.);
#10151=ORIENTED_EDGE('',*,*,#7076,.F.);
#10152=ORIENTED_EDGE('',*,*,#7255,.F.);
#10153=ORIENTED_EDGE('',*,*,#7048,.F.);
#10154=ORIENTED_EDGE('',*,*,#7254,.F.);
#10155=ORIENTED_EDGE('',*,*,#7078,.F.);
#10156=ORIENTED_EDGE('',*,*,#7252,.T.);
#10157=ORIENTED_EDGE('',*,*,#7060,.F.);
#10158=ORIENTED_EDGE('',*,*,#7256,.F.);
#10159=ORIENTED_EDGE('',*,*,#7063,.F.);
#10160=ORIENTED_EDGE('',*,*,#7257,.T.);
#10161=ORIENTED_EDGE('',*,*,#7058,.F.);
#10162=ORIENTED_EDGE('',*,*,#7258,.T.);
#10163=ORIENTED_EDGE('',*,*,#7065,.F.);
#10164=ORIENTED_EDGE('',*,*,#7259,.F.);
#10165=ORIENTED_EDGE('',*,*,#7061,.F.);
#10166=ORIENTED_EDGE('',*,*,#7257,.F.);
#10167=ORIENTED_EDGE('',*,*,#7062,.F.);
#10168=ORIENTED_EDGE('',*,*,#7055,.F.);
#10169=ORIENTED_EDGE('',*,*,#7258,.F.);
#10170=ORIENTED_EDGE('',*,*,#7057,.F.);
#10171=ORIENTED_EDGE('',*,*,#7256,.T.);
#10172=ORIENTED_EDGE('',*,*,#7059,.T.);
#10173=ORIENTED_EDGE('',*,*,#7259,.T.);
#10174=ORIENTED_EDGE('',*,*,#7064,.T.);
#10175=ORIENTED_EDGE('',*,*,#7046,.F.);
#10176=ORIENTED_EDGE('',*,*,#7066,.T.);
#10177=ORIENTED_EDGE('',*,*,#7044,.T.);
#10178=ORIENTED_EDGE('',*,*,#7067,.F.);
#10179=ORIENTED_EDGE('',*,*,#7206,.F.);
#10180=ORIENTED_EDGE('',*,*,#7260,.F.);
#10181=ORIENTED_EDGE('',*,*,#7053,.F.);
#10182=ORIENTED_EDGE('',*,*,#7261,.F.);
#10183=ORIENTED_EDGE('',*,*,#7262,.T.);
#10184=ORIENTED_EDGE('',*,*,#7204,.T.);
#10185=ORIENTED_EDGE('',*,*,#7263,.T.);
#10186=ORIENTED_EDGE('',*,*,#7051,.T.);
#10187=ORIENTED_EDGE('',*,*,#7207,.F.);
#10188=ORIENTED_EDGE('',*,*,#7261,.T.);
#10189=ORIENTED_EDGE('',*,*,#7052,.F.);
#10190=ORIENTED_EDGE('',*,*,#7263,.F.);
#10191=ORIENTED_EDGE('',*,*,#7205,.F.);
#10192=ORIENTED_EDGE('',*,*,#7262,.F.);
#10193=ORIENTED_EDGE('',*,*,#7054,.F.);
#10194=ORIENTED_EDGE('',*,*,#7260,.T.);
#10195=ORIENTED_EDGE('',*,*,#7177,.F.);
#10196=ORIENTED_EDGE('',*,*,#7264,.T.);
#10197=ORIENTED_EDGE('',*,*,#7183,.T.);
#10198=ORIENTED_EDGE('',*,*,#7265,.T.);
#10199=ORIENTED_EDGE('',*,*,#7266,.F.);
#10200=ORIENTED_EDGE('',*,*,#7175,.T.);
#10201=ORIENTED_EDGE('',*,*,#7179,.T.);
#10202=ORIENTED_EDGE('',*,*,#7267,.F.);
#10203=ORIENTED_EDGE('',*,*,#7181,.F.);
#10204=ORIENTED_EDGE('',*,*,#7185,.F.);
#10205=ORIENTED_EDGE('',*,*,#7267,.T.);
#10206=ORIENTED_EDGE('',*,*,#7178,.T.);
#10207=ORIENTED_EDGE('',*,*,#7265,.F.);
#10208=ORIENTED_EDGE('',*,*,#7182,.F.);
#10209=ORIENTED_EDGE('',*,*,#7264,.F.);
#10210=ORIENTED_EDGE('',*,*,#7176,.T.);
#10211=ORIENTED_EDGE('',*,*,#7266,.T.);
#10212=ORIENTED_EDGE('',*,*,#7184,.F.);
#12143=CYLINDRICAL_SURFACE('',#13645,7.5);
#12144=CYLINDRICAL_SURFACE('',#13648,12.4653846153846);
#12145=CYLINDRICAL_SURFACE('',#13650,12.4653846153846);
#12146=CYLINDRICAL_SURFACE('',#13686,17.6897435897436);
#12147=CYLINDRICAL_SURFACE('',#13689,16.2686153846154);
#12148=CYLINDRICAL_SURFACE('',#13691,16.0346153846154);
#12149=CYLINDRICAL_SURFACE('',#13696,16.0346153846154);
#12150=CYLINDRICAL_SURFACE('',#13697,16.2686153846154);
#12151=CYLINDRICAL_SURFACE('',#13699,17.6897435897436);
#12152=CYLINDRICAL_SURFACE('',#13709,21.);
#12153=CYLINDRICAL_SURFACE('',#13814,14.25);
#12154=CYLINDRICAL_SURFACE('',#13817,15.1423076923077);
#12155=CYLINDRICAL_SURFACE('',#13830,15.1423076923077);
#12156=CYLINDRICAL_SURFACE('',#13831,14.25);
#12157=CYLINDRICAL_SURFACE('',#13840,15.1423076923077);
#12158=CYLINDRICAL_SURFACE('',#13841,14.25);
#12159=CYLINDRICAL_SURFACE('',#13842,14.25);
#12160=CYLINDRICAL_SURFACE('',#13845,15.1423076923077);
#12161=CYLINDRICAL_SURFACE('',#13858,15.1423076923077);
#12162=CYLINDRICAL_SURFACE('',#13859,14.25);
#12163=CYLINDRICAL_SURFACE('',#13860,14.25);
#12164=CYLINDRICAL_SURFACE('',#13863,15.1423076923077);
#12165=CYLINDRICAL_SURFACE('',#13876,15.1423076923077);
#12166=CYLINDRICAL_SURFACE('',#13877,14.25);
#12167=CYLINDRICAL_SURFACE('',#13878,14.25);
#12168=CYLINDRICAL_SURFACE('',#13881,15.1423076923077);
#12169=CYLINDRICAL_SURFACE('',#13894,15.1423076923077);
#12170=CYLINDRICAL_SURFACE('',#13895,14.25);
#12171=CYLINDRICAL_SURFACE('',#13896,14.25);
#12172=CYLINDRICAL_SURFACE('',#13899,15.1423076923077);
#12173=CYLINDRICAL_SURFACE('',#13912,15.1423076923077);
#12174=CYLINDRICAL_SURFACE('',#13913,14.25);
#12175=CYLINDRICAL_SURFACE('',#13914,14.25);
#12176=CYLINDRICAL_SURFACE('',#13917,15.1423076923077);
#12177=CYLINDRICAL_SURFACE('',#13930,15.1423076923077);
#12178=CYLINDRICAL_SURFACE('',#13931,14.25);
#12179=CYLINDRICAL_SURFACE('',#13938,15.1423076923077);
#12180=CYLINDRICAL_SURFACE('',#13939,14.25);
#12551=ADVANCED_FACE('',(#1539),#115,.F.);
#12552=ADVANCED_FACE('',(#1540),#116,.T.);
#12553=ADVANCED_FACE('',(#1541),#117,.T.);
#12554=ADVANCED_FACE('',(#1542),#99,.F.);
#12555=ADVANCED_FACE('',(#1543),#12143,.F.);
#12556=ADVANCED_FACE('',(#1544),#100,.F.);
#12557=ADVANCED_FACE('',(#1545),#12144,.T.);
#12558=ADVANCED_FACE('',(#1546),#12145,.T.);
#12559=ADVANCED_FACE('',(#1547,#283),#1075,.F.);
#12560=ADVANCED_FACE('',(#1548,#284),#1076,.F.);
#12561=ADVANCED_FACE('',(#1549),#43,.T.);
#12562=ADVANCED_FACE('',(#1550),#44,.T.);
#12563=ADVANCED_FACE('',(#1551),#45,.T.);
#12564=ADVANCED_FACE('',(#1552),#46,.T.);
#12565=ADVANCED_FACE('',(#1553),#47,.T.);
#12566=ADVANCED_FACE('',(#1554),#48,.T.);
#12567=ADVANCED_FACE('',(#1555),#49,.T.);
#12568=ADVANCED_FACE('',(#1556),#118,.T.);
#12569=ADVANCED_FACE('',(#1557),#119,.T.);
#12570=ADVANCED_FACE('',(#1558),#120,.T.);
#12571=ADVANCED_FACE('',(#1559),#121,.T.);
#12572=ADVANCED_FACE('',(#1560),#12146,.F.);
#12573=ADVANCED_FACE('',(#1561),#12147,.F.);
#12574=ADVANCED_FACE('',(#1562),#12148,.F.);
#12575=ADVANCED_FACE('',(#1563),#122,.F.);
#12576=ADVANCED_FACE('',(#1564),#12149,.F.);
#12577=ADVANCED_FACE('',(#1565),#12150,.F.);
#12578=ADVANCED_FACE('',(#1566),#12151,.F.);
#12579=ADVANCED_FACE('',(#1567),#101,.T.);
#12580=ADVANCED_FACE('',(#1568),#102,.T.);
#12581=ADVANCED_FACE('',(#1569),#12152,.T.);
#12582=ADVANCED_FACE('',(#1570,#285),#1077,.F.);
#12583=ADVANCED_FACE('',(#1571,#286),#1078,.F.);
#12584=ADVANCED_FACE('',(#1572,#287),#1079,.T.);
#12585=ADVANCED_FACE('',(#1573,#288),#1080,.T.);
#12586=ADVANCED_FACE('',(#1574,#289),#1081,.T.);
#12587=ADVANCED_FACE('',(#1575,#290),#1082,.T.);
#12588=ADVANCED_FACE('',(#1576,#291,#292),#123,.T.);
#12589=ADVANCED_FACE('',(#1577,#293,#294),#50,.F.);
#12590=ADVANCED_FACE('',(#1578,#295,#296),#124,.T.);
#12591=ADVANCED_FACE('',(#1579,#297,#298),#51,.F.);
#12592=ADVANCED_FACE('',(#1580,#299,#300),#125,.T.);
#12593=ADVANCED_FACE('',(#1581,#301,#302),#52,.F.);
#12594=ADVANCED_FACE('',(#1582,#303,#304),#126,.T.);
#12595=ADVANCED_FACE('',(#1583,#305,#306),#53,.F.);
#12596=ADVANCED_FACE('',(#1584,#307,#308),#127,.T.);
#12597=ADVANCED_FACE('',(#1585,#309,#310),#54,.F.);
#12598=ADVANCED_FACE('',(#1586,#311,#312),#128,.T.);
#12599=ADVANCED_FACE('',(#1587,#313,#314),#55,.F.);
#12600=ADVANCED_FACE('',(#1588,#315,#316),#56,.F.);
#12601=ADVANCED_FACE('',(#1589,#317,#318),#129,.T.);
#12602=ADVANCED_FACE('',(#1590),#12153,.F.);
#12603=ADVANCED_FACE('',(#1591),#12154,.T.);
#12604=ADVANCED_FACE('',(#1592),#1083,.T.);
#12605=ADVANCED_FACE('',(#1593),#1084,.F.);
#12606=ADVANCED_FACE('',(#1594,#319),#1085,.T.);
#12607=ADVANCED_FACE('',(#1595,#320),#1086,.T.);
#12608=ADVANCED_FACE('',(#1596),#1087,.T.);
#12609=ADVANCED_FACE('',(#1597),#1088,.F.);
#12610=ADVANCED_FACE('',(#1598),#12155,.T.);
#12611=ADVANCED_FACE('',(#1599),#12156,.F.);
#12612=ADVANCED_FACE('',(#1600,#321),#1089,.T.);
#12613=ADVANCED_FACE('',(#1601,#322),#1090,.T.);
#12614=ADVANCED_FACE('',(#1602),#1091,.F.);
#12615=ADVANCED_FACE('',(#1603),#1092,.T.);
#12616=ADVANCED_FACE('',(#1604),#12157,.T.);
#12617=ADVANCED_FACE('',(#1605),#12158,.F.);
#12618=ADVANCED_FACE('',(#1606),#12159,.F.);
#12619=ADVANCED_FACE('',(#1607),#12160,.T.);
#12620=ADVANCED_FACE('',(#1608),#1093,.F.);
#12621=ADVANCED_FACE('',(#1609),#1094,.T.);
#12622=ADVANCED_FACE('',(#1610,#323),#1095,.T.);
#12623=ADVANCED_FACE('',(#1611,#324),#1096,.T.);
#12624=ADVANCED_FACE('',(#1612),#1097,.F.);
#12625=ADVANCED_FACE('',(#1613),#1098,.T.);
#12626=ADVANCED_FACE('',(#1614),#12161,.T.);
#12627=ADVANCED_FACE('',(#1615),#12162,.F.);
#12628=ADVANCED_FACE('',(#1616),#12163,.F.);
#12629=ADVANCED_FACE('',(#1617),#12164,.T.);
#12630=ADVANCED_FACE('',(#1618),#1099,.F.);
#12631=ADVANCED_FACE('',(#1619),#1100,.T.);
#12632=ADVANCED_FACE('',(#1620,#325),#1101,.T.);
#12633=ADVANCED_FACE('',(#1621,#326),#1102,.T.);
#12634=ADVANCED_FACE('',(#1622),#1103,.F.);
#12635=ADVANCED_FACE('',(#1623),#1104,.T.);
#12636=ADVANCED_FACE('',(#1624),#12165,.T.);
#12637=ADVANCED_FACE('',(#1625),#12166,.F.);
#12638=ADVANCED_FACE('',(#1626),#12167,.F.);
#12639=ADVANCED_FACE('',(#1627),#12168,.T.);
#12640=ADVANCED_FACE('',(#1628),#1105,.F.);
#12641=ADVANCED_FACE('',(#1629),#1106,.T.);
#12642=ADVANCED_FACE('',(#1630,#327),#1107,.T.);
#12643=ADVANCED_FACE('',(#1631,#328),#1108,.T.);
#12644=ADVANCED_FACE('',(#1632),#1109,.F.);
#12645=ADVANCED_FACE('',(#1633),#1110,.T.);
#12646=ADVANCED_FACE('',(#1634),#12169,.T.);
#12647=ADVANCED_FACE('',(#1635),#12170,.F.);
#12648=ADVANCED_FACE('',(#1636),#12171,.F.);
#12649=ADVANCED_FACE('',(#1637),#12172,.T.);
#12650=ADVANCED_FACE('',(#1638),#1111,.F.);
#12651=ADVANCED_FACE('',(#1639),#1112,.T.);
#12652=ADVANCED_FACE('',(#1640,#329),#1113,.T.);
#12653=ADVANCED_FACE('',(#1641,#330),#1114,.T.);
#12654=ADVANCED_FACE('',(#1642),#1115,.F.);
#12655=ADVANCED_FACE('',(#1643),#1116,.T.);
#12656=ADVANCED_FACE('',(#1644),#12173,.T.);
#12657=ADVANCED_FACE('',(#1645),#12174,.F.);
#12658=ADVANCED_FACE('',(#1646),#12175,.F.);
#12659=ADVANCED_FACE('',(#1647),#12176,.T.);
#12660=ADVANCED_FACE('',(#1648),#1117,.F.);
#12661=ADVANCED_FACE('',(#1649),#1118,.T.);
#12662=ADVANCED_FACE('',(#1650,#331),#1119,.T.);
#12663=ADVANCED_FACE('',(#1651,#332),#1120,.T.);
#12664=ADVANCED_FACE('',(#1652),#1121,.F.);
#12665=ADVANCED_FACE('',(#1653),#1122,.T.);
#12666=ADVANCED_FACE('',(#1654),#12177,.T.);
#12667=ADVANCED_FACE('',(#1655),#12178,.F.);
#12668=ADVANCED_FACE('',(#1656),#1123,.T.);
#12669=ADVANCED_FACE('',(#1657),#1124,.F.);
#12670=ADVANCED_FACE('',(#1658),#12179,.T.);
#12671=ADVANCED_FACE('',(#1659),#12180,.F.);
#13053=CLOSED_SHELL('',(#12551,#12552,#12553,#12554,#12555,#12556,#12557,
#12558,#12559,#12560));
#13054=CLOSED_SHELL('',(#12561));
#13055=CLOSED_SHELL('',(#12562));
#13056=CLOSED_SHELL('',(#12563));
#13057=CLOSED_SHELL('',(#12564));
#13058=CLOSED_SHELL('',(#12565));
#13059=CLOSED_SHELL('',(#12566));
#13060=CLOSED_SHELL('',(#12567));
#13061=CLOSED_SHELL('',(#12568,#12569,#12570,#12571,#12572,#12573,#12574,
#12575,#12576,#12577,#12578,#12579,#12580,#12581,#12582,#12583,#12584,#12585,
#12586,#12587));
#13062=CLOSED_SHELL('',(#12588,#12589,#12590,#12591,#12592,#12593,#12594,
#12595,#12596,#12597,#12598,#12599,#12600,#12601,#12602,#12603,#12604,#12605,
#12606,#12607,#12608,#12609,#12610,#12611,#12612,#12613,#12614,#12615,#12616,
#12617,#12618,#12619,#12620,#12621,#12622,#12623,#12624,#12625,#12626,#12627,
#12628,#12629,#12630,#12631,#12632,#12633,#12634,#12635,#12636,#12637,#12638,
#12639,#12640,#12641,#12642,#12643,#12644,#12645,#12646,#12647,#12648,#12649,
#12650,#12651,#12652,#12653,#12654,#12655,#12656,#12657,#12658,#12659,#12660,
#12661,#12662,#12663,#12664,#12665,#12666,#12667,#12668,#12669,#12670,#12671));
#13627=AXIS2_PLACEMENT_3D('',#38024,#16163,#16164);
#13628=AXIS2_PLACEMENT_3D('',#38025,#16165,#16166);
#13629=AXIS2_PLACEMENT_3D('',#38027,#16167,#16168);
#13630=AXIS2_PLACEMENT_3D('',#38029,#16169,#16170);
#13631=AXIS2_PLACEMENT_3D('',#38030,#16171,#16172);
#13632=AXIS2_PLACEMENT_3D('',#38031,#16173,#16174);
#13633=AXIS2_PLACEMENT_3D('',#38034,#16175,#16176);
#13634=AXIS2_PLACEMENT_3D('',#38035,#16177,#16178);
#13635=AXIS2_PLACEMENT_3D('',#38037,#16179,#16180);
#13636=AXIS2_PLACEMENT_3D('',#38039,#16181,#16182);
#13637=AXIS2_PLACEMENT_3D('',#38040,#16183,#16184);
#13638=AXIS2_PLACEMENT_3D('',#38041,#16185,#16186);
#13639=AXIS2_PLACEMENT_3D('',#38044,#16187,#16188);
#13640=AXIS2_PLACEMENT_3D('',#38045,#16189,#16190);
#13641=AXIS2_PLACEMENT_3D('',#38047,#16191,#16192);
#13642=AXIS2_PLACEMENT_3D('',#38048,#16193,#16194);
#13643=AXIS2_PLACEMENT_3D('',#38049,#16195,#16196);
#13644=AXIS2_PLACEMENT_3D('',#38052,#16198,#16199);
#13645=AXIS2_PLACEMENT_3D('',#38053,#16200,#16201);
#13646=AXIS2_PLACEMENT_3D('',#38055,#16203,#16204);
#13647=AXIS2_PLACEMENT_3D('',#38058,#16206,#16207);
#13648=AXIS2_PLACEMENT_3D('',#38059,#16208,#16209);
#13649=AXIS2_PLACEMENT_3D('',#38062,#16211,#16212);
#13650=AXIS2_PLACEMENT_3D('',#38063,#16213,#16214);
#13651=AXIS2_PLACEMENT_3D('',#38065,#16215,#16216);
#13652=AXIS2_PLACEMENT_3D('',#38067,#16218,#16219);
#13653=AXIS2_PLACEMENT_3D('',#38068,#16220,#16221);
#13654=AXIS2_PLACEMENT_3D('',#38069,#16222,#16223);
#13655=AXIS2_PLACEMENT_3D('',#38072,#16224,#16225);
#13656=AXIS2_PLACEMENT_3D('',#38073,#16226,#16227);
#13657=AXIS2_PLACEMENT_3D('',#38076,#16228,#16229);
#13658=AXIS2_PLACEMENT_3D('',#38077,#16230,#16231);
#13659=AXIS2_PLACEMENT_3D('',#38080,#16232,#16233);
#13660=AXIS2_PLACEMENT_3D('',#38081,#16234,#16235);
#13661=AXIS2_PLACEMENT_3D('',#38084,#16236,#16237);
#13662=AXIS2_PLACEMENT_3D('',#38085,#16238,#16239);
#13663=AXIS2_PLACEMENT_3D('',#38088,#16240,#16241);
#13664=AXIS2_PLACEMENT_3D('',#38089,#16242,#16243);
#13665=AXIS2_PLACEMENT_3D('',#38092,#16244,#16245);
#13666=AXIS2_PLACEMENT_3D('',#38093,#16246,#16247);
#13667=AXIS2_PLACEMENT_3D('',#38096,#16248,#16249);
#13668=AXIS2_PLACEMENT_3D('',#38097,#16250,#16251);
#13669=AXIS2_PLACEMENT_3D('',#38099,#16252,#16253);
#13670=AXIS2_PLACEMENT_3D('',#38101,#16254,#16255);
#13671=AXIS2_PLACEMENT_3D('',#38103,#16256,#16257);
#13672=AXIS2_PLACEMENT_3D('',#38104,#16258,#16259);
#13673=AXIS2_PLACEMENT_3D('',#38105,#16260,#16261);
#13674=AXIS2_PLACEMENT_3D('',#38107,#16262,#16263);
#13675=AXIS2_PLACEMENT_3D('',#38109,#16264,#16265);
#13676=AXIS2_PLACEMENT_3D('',#38110,#16266,#16267);
#13677=AXIS2_PLACEMENT_3D('',#38111,#16268,#16269);
#13678=AXIS2_PLACEMENT_3D('',#38113,#16270,#16271);
#13679=AXIS2_PLACEMENT_3D('',#38115,#16272,#16273);
#13680=AXIS2_PLACEMENT_3D('',#38116,#16274,#16275);
#13681=AXIS2_PLACEMENT_3D('',#38117,#16276,#16277);
#13682=AXIS2_PLACEMENT_3D('',#38120,#16278,#16279);
#13683=AXIS2_PLACEMENT_3D('',#38121,#16280,#16281);
#13684=AXIS2_PLACEMENT_3D('',#38123,#16282,#16283);
#13685=AXIS2_PLACEMENT_3D('',#38124,#16284,#16285);
#13686=AXIS2_PLACEMENT_3D('',#38125,#16286,#16287);
#13687=AXIS2_PLACEMENT_3D('',#38127,#16288,#16289);
#13688=AXIS2_PLACEMENT_3D('',#38130,#16291,#16292);
#13689=AXIS2_PLACEMENT_3D('',#38131,#16293,#16294);
#13690=AXIS2_PLACEMENT_3D('',#38133,#16295,#16296);
#13691=AXIS2_PLACEMENT_3D('',#38135,#16298,#16299);
#13692=AXIS2_PLACEMENT_3D('',#38138,#16301,#16302);
#13693=AXIS2_PLACEMENT_3D('',#38139,#16303,#16304);
#13694=AXIS2_PLACEMENT_3D('',#38141,#16305,#16306);
#13695=AXIS2_PLACEMENT_3D('',#38142,#16307,#16308);
#13696=AXIS2_PLACEMENT_3D('',#38143,#16309,#16310);
#13697=AXIS2_PLACEMENT_3D('',#38145,#16312,#16313);
#13698=AXIS2_PLACEMENT_3D('',#38148,#16315,#16316);
#13699=AXIS2_PLACEMENT_3D('',#38149,#16317,#16318);
#13700=AXIS2_PLACEMENT_3D('',#38151,#16319,#16320);
#13701=AXIS2_PLACEMENT_3D('',#38154,#16322,#16323);
#13702=AXIS2_PLACEMENT_3D('',#38155,#16324,#16325);
#13703=AXIS2_PLACEMENT_3D('',#38157,#16326,#16327);
#13704=AXIS2_PLACEMENT_3D('',#38160,#16329,#16330);
#13705=AXIS2_PLACEMENT_3D('',#38161,#16331,#16332);
#13706=AXIS2_PLACEMENT_3D('',#38164,#16333,#16334);
#13707=AXIS2_PLACEMENT_3D('',#38167,#16336,#16337);
#13708=AXIS2_PLACEMENT_3D('',#38168,#16338,#16339);
#13709=AXIS2_PLACEMENT_3D('',#38169,#16340,#16341);
#13710=AXIS2_PLACEMENT_3D('',#38171,#16343,#16344);
#13711=AXIS2_PLACEMENT_3D('',#38172,#16345,#16346);
#13712=AXIS2_PLACEMENT_3D('',#38173,#16347,#16348);
#13713=AXIS2_PLACEMENT_3D('',#38174,#16349,#16350);
#13714=AXIS2_PLACEMENT_3D('',#38175,#16351,#16352);
#13715=AXIS2_PLACEMENT_3D('',#38176,#16353,#16354);
#13716=AXIS2_PLACEMENT_3D('',#38177,#16355,#16356);
#13717=AXIS2_PLACEMENT_3D('',#38179,#16357,#16358);
#13718=AXIS2_PLACEMENT_3D('',#38181,#16359,#16360);
#13719=AXIS2_PLACEMENT_3D('',#38182,#16361,#16362);
#13720=AXIS2_PLACEMENT_3D('',#38291,#16363,#16364);
#13721=AXIS2_PLACEMENT_3D('',#38294,#16365,#16366);
#13722=AXIS2_PLACEMENT_3D('',#38296,#16367,#16368);
#13723=AXIS2_PLACEMENT_3D('',#38298,#16369,#16370);
#13724=AXIS2_PLACEMENT_3D('',#38308,#16371,#16372);
#13725=AXIS2_PLACEMENT_3D('',#38317,#16373,#16374);
#13726=AXIS2_PLACEMENT_3D('',#38319,#16375,#16376);
#13727=AXIS2_PLACEMENT_3D('',#38328,#16377,#16378);
#13728=AXIS2_PLACEMENT_3D('',#38336,#16379,#16380);
#13729=AXIS2_PLACEMENT_3D('',#38338,#16381,#16382);
#13730=AXIS2_PLACEMENT_3D('',#38339,#16383,#16384);
#13731=AXIS2_PLACEMENT_3D('',#38341,#16385,#16386);
#13732=AXIS2_PLACEMENT_3D('',#38343,#16387,#16388);
#13733=AXIS2_PLACEMENT_3D('',#38344,#16389,#16390);
#13734=AXIS2_PLACEMENT_3D('',#38453,#16391,#16392);
#13735=AXIS2_PLACEMENT_3D('',#38456,#16393,#16394);
#13736=AXIS2_PLACEMENT_3D('',#38458,#16395,#16396);
#13737=AXIS2_PLACEMENT_3D('',#38460,#16397,#16398);
#13738=AXIS2_PLACEMENT_3D('',#38470,#16399,#16400);
#13739=AXIS2_PLACEMENT_3D('',#38479,#16401,#16402);
#13740=AXIS2_PLACEMENT_3D('',#38481,#16403,#16404);
#13741=AXIS2_PLACEMENT_3D('',#38490,#16405,#16406);
#13742=AXIS2_PLACEMENT_3D('',#38498,#16407,#16408);
#13743=AXIS2_PLACEMENT_3D('',#38500,#16409,#16410);
#13744=AXIS2_PLACEMENT_3D('',#38501,#16411,#16412);
#13745=AXIS2_PLACEMENT_3D('',#38503,#16413,#16414);
#13746=AXIS2_PLACEMENT_3D('',#38505,#16415,#16416);
#13747=AXIS2_PLACEMENT_3D('',#38506,#16417,#16418);
#13748=AXIS2_PLACEMENT_3D('',#38615,#16419,#16420);
#13749=AXIS2_PLACEMENT_3D('',#38618,#16421,#16422);
#13750=AXIS2_PLACEMENT_3D('',#38620,#16423,#16424);
#13751=AXIS2_PLACEMENT_3D('',#38622,#16425,#16426);
#13752=AXIS2_PLACEMENT_3D('',#38632,#16427,#16428);
#13753=AXIS2_PLACEMENT_3D('',#38641,#16429,#16430);
#13754=AXIS2_PLACEMENT_3D('',#38643,#16431,#16432);
#13755=AXIS2_PLACEMENT_3D('',#38652,#16433,#16434);
#13756=AXIS2_PLACEMENT_3D('',#38660,#16435,#16436);
#13757=AXIS2_PLACEMENT_3D('',#38662,#16437,#16438);
#13758=AXIS2_PLACEMENT_3D('',#38663,#16439,#16440);
#13759=AXIS2_PLACEMENT_3D('',#38665,#16441,#16442);
#13760=AXIS2_PLACEMENT_3D('',#38667,#16443,#16444);
#13761=AXIS2_PLACEMENT_3D('',#38668,#16445,#16446);
#13762=AXIS2_PLACEMENT_3D('',#38777,#16447,#16448);
#13763=AXIS2_PLACEMENT_3D('',#38780,#16449,#16450);
#13764=AXIS2_PLACEMENT_3D('',#38782,#16451,#16452);
#13765=AXIS2_PLACEMENT_3D('',#38784,#16453,#16454);
#13766=AXIS2_PLACEMENT_3D('',#38794,#16455,#16456);
#13767=AXIS2_PLACEMENT_3D('',#38803,#16457,#16458);
#13768=AXIS2_PLACEMENT_3D('',#38805,#16459,#16460);
#13769=AXIS2_PLACEMENT_3D('',#38814,#16461,#16462);
#13770=AXIS2_PLACEMENT_3D('',#38822,#16463,#16464);
#13771=AXIS2_PLACEMENT_3D('',#38824,#16465,#16466);
#13772=AXIS2_PLACEMENT_3D('',#38825,#16467,#16468);
#13773=AXIS2_PLACEMENT_3D('',#38827,#16469,#16470);
#13774=AXIS2_PLACEMENT_3D('',#38829,#16471,#16472);
#13775=AXIS2_PLACEMENT_3D('',#38830,#16473,#16474);
#13776=AXIS2_PLACEMENT_3D('',#38939,#16475,#16476);
#13777=AXIS2_PLACEMENT_3D('',#38942,#16477,#16478);
#13778=AXIS2_PLACEMENT_3D('',#38944,#16479,#16480);
#13779=AXIS2_PLACEMENT_3D('',#38946,#16481,#16482);
#13780=AXIS2_PLACEMENT_3D('',#38956,#16483,#16484);
#13781=AXIS2_PLACEMENT_3D('',#38965,#16485,#16486);
#13782=AXIS2_PLACEMENT_3D('',#38967,#16487,#16488);
#13783=AXIS2_PLACEMENT_3D('',#38976,#16489,#16490);
#13784=AXIS2_PLACEMENT_3D('',#38984,#16491,#16492);
#13785=AXIS2_PLACEMENT_3D('',#38986,#16493,#16494);
#13786=AXIS2_PLACEMENT_3D('',#38987,#16495,#16496);
#13787=AXIS2_PLACEMENT_3D('',#38989,#16497,#16498);
#13788=AXIS2_PLACEMENT_3D('',#38991,#16499,#16500);
#13789=AXIS2_PLACEMENT_3D('',#38992,#16501,#16502);
#13790=AXIS2_PLACEMENT_3D('',#39101,#16503,#16504);
#13791=AXIS2_PLACEMENT_3D('',#39104,#16505,#16506);
#13792=AXIS2_PLACEMENT_3D('',#39113,#16507,#16508);
#13793=AXIS2_PLACEMENT_3D('',#39121,#16509,#16510);
#13794=AXIS2_PLACEMENT_3D('',#39123,#16511,#16512);
#13795=AXIS2_PLACEMENT_3D('',#39125,#16513,#16514);
#13796=AXIS2_PLACEMENT_3D('',#39135,#16515,#16516);
#13797=AXIS2_PLACEMENT_3D('',#39144,#16517,#16518);
#13798=AXIS2_PLACEMENT_3D('',#39146,#16519,#16520);
#13799=AXIS2_PLACEMENT_3D('',#39148,#16521,#16522);
#13800=AXIS2_PLACEMENT_3D('',#39149,#16523,#16524);
#13801=AXIS2_PLACEMENT_3D('',#39152,#16525,#16526);
#13802=AXIS2_PLACEMENT_3D('',#39154,#16527,#16528);
#13803=AXIS2_PLACEMENT_3D('',#39156,#16529,#16530);
#13804=AXIS2_PLACEMENT_3D('',#39166,#16531,#16532);
#13805=AXIS2_PLACEMENT_3D('',#39175,#16533,#16534);
#13806=AXIS2_PLACEMENT_3D('',#39177,#16535,#16536);
#13807=AXIS2_PLACEMENT_3D('',#39186,#16537,#16538);
#13808=AXIS2_PLACEMENT_3D('',#39194,#16539,#16540);
#13809=AXIS2_PLACEMENT_3D('',#39196,#16541,#16542);
#13810=AXIS2_PLACEMENT_3D('',#39197,#16543,#16544);
#13811=AXIS2_PLACEMENT_3D('',#39199,#16545,#16546);
#13812=AXIS2_PLACEMENT_3D('',#39201,#16547,#16548);
#13813=AXIS2_PLACEMENT_3D('',#39202,#16549,#16550);
#13814=AXIS2_PLACEMENT_3D('',#39311,#16551,#16552);
#13815=AXIS2_PLACEMENT_3D('',#39312,#16553,#16554);
#13816=AXIS2_PLACEMENT_3D('',#39313,#16555,#16556);
#13817=AXIS2_PLACEMENT_3D('',#39314,#16557,#16558);
#13818=AXIS2_PLACEMENT_3D('',#39315,#16559,#16560);
#13819=AXIS2_PLACEMENT_3D('',#39316,#16561,#16562);
#13820=AXIS2_PLACEMENT_3D('',#39317,#16563,#16564);
#13821=AXIS2_PLACEMENT_3D('',#39318,#16565,#16566);
#13822=AXIS2_PLACEMENT_3D('',#39319,#16567,#16568);
#13823=AXIS2_PLACEMENT_3D('',#39320,#16569,#16570);
#13824=AXIS2_PLACEMENT_3D('',#39321,#16571,#16572);
#13825=AXIS2_PLACEMENT_3D('',#39322,#16573,#16574);
#13826=AXIS2_PLACEMENT_3D('',#39323,#16575,#16576);
#13827=AXIS2_PLACEMENT_3D('',#39324,#16577,#16578);
#13828=AXIS2_PLACEMENT_3D('',#39325,#16579,#16580);
#13829=AXIS2_PLACEMENT_3D('',#39326,#16581,#16582);
#13830=AXIS2_PLACEMENT_3D('',#39327,#16583,#16584);
#13831=AXIS2_PLACEMENT_3D('',#39328,#16585,#16586);
#13832=AXIS2_PLACEMENT_3D('',#39329,#16587,#16588);
#13833=AXIS2_PLACEMENT_3D('',#39330,#16589,#16590);
#13834=AXIS2_PLACEMENT_3D('',#39331,#16591,#16592);
#13835=AXIS2_PLACEMENT_3D('',#39332,#16593,#16594);
#13836=AXIS2_PLACEMENT_3D('',#39333,#16595,#16596);
#13837=AXIS2_PLACEMENT_3D('',#39334,#16597,#16598);
#13838=AXIS2_PLACEMENT_3D('',#39335,#16599,#16600);
#13839=AXIS2_PLACEMENT_3D('',#39336,#16601,#16602);
#13840=AXIS2_PLACEMENT_3D('',#39337,#16603,#16604);
#13841=AXIS2_PLACEMENT_3D('',#39338,#16605,#16606);
#13842=AXIS2_PLACEMENT_3D('',#39339,#16607,#16608);
#13843=AXIS2_PLACEMENT_3D('',#39340,#16609,#16610);
#13844=AXIS2_PLACEMENT_3D('',#39341,#16611,#16612);
#13845=AXIS2_PLACEMENT_3D('',#39342,#16613,#16614);
#13846=AXIS2_PLACEMENT_3D('',#39343,#16615,#16616);
#13847=AXIS2_PLACEMENT_3D('',#39344,#16617,#16618);
#13848=AXIS2_PLACEMENT_3D('',#39345,#16619,#16620);
#13849=AXIS2_PLACEMENT_3D('',#39346,#16621,#16622);
#13850=AXIS2_PLACEMENT_3D('',#39347,#16623,#16624);
#13851=AXIS2_PLACEMENT_3D('',#39348,#16625,#16626);
#13852=AXIS2_PLACEMENT_3D('',#39349,#16627,#16628);
#13853=AXIS2_PLACEMENT_3D('',#39350,#16629,#16630);
#13854=AXIS2_PLACEMENT_3D('',#39351,#16631,#16632);
#13855=AXIS2_PLACEMENT_3D('',#39352,#16633,#16634);
#13856=AXIS2_PLACEMENT_3D('',#39353,#16635,#16636);
#13857=AXIS2_PLACEMENT_3D('',#39354,#16637,#16638);
#13858=AXIS2_PLACEMENT_3D('',#39355,#16639,#16640);
#13859=AXIS2_PLACEMENT_3D('',#39356,#16641,#16642);
#13860=AXIS2_PLACEMENT_3D('',#39357,#16643,#16644);
#13861=AXIS2_PLACEMENT_3D('',#39358,#16645,#16646);
#13862=AXIS2_PLACEMENT_3D('',#39359,#16647,#16648);
#13863=AXIS2_PLACEMENT_3D('',#39360,#16649,#16650);
#13864=AXIS2_PLACEMENT_3D('',#39361,#16651,#16652);
#13865=AXIS2_PLACEMENT_3D('',#39362,#16653,#16654);
#13866=AXIS2_PLACEMENT_3D('',#39363,#16655,#16656);
#13867=AXIS2_PLACEMENT_3D('',#39364,#16657,#16658);
#13868=AXIS2_PLACEMENT_3D('',#39365,#16659,#16660);
#13869=AXIS2_PLACEMENT_3D('',#39366,#16661,#16662);
#13870=AXIS2_PLACEMENT_3D('',#39367,#16663,#16664);
#13871=AXIS2_PLACEMENT_3D('',#39368,#16665,#16666);
#13872=AXIS2_PLACEMENT_3D('',#39369,#16667,#16668);
#13873=AXIS2_PLACEMENT_3D('',#39370,#16669,#16670);
#13874=AXIS2_PLACEMENT_3D('',#39371,#16671,#16672);
#13875=AXIS2_PLACEMENT_3D('',#39372,#16673,#16674);
#13876=AXIS2_PLACEMENT_3D('',#39373,#16675,#16676);
#13877=AXIS2_PLACEMENT_3D('',#39374,#16677,#16678);
#13878=AXIS2_PLACEMENT_3D('',#39375,#16679,#16680);
#13879=AXIS2_PLACEMENT_3D('',#39376,#16681,#16682);
#13880=AXIS2_PLACEMENT_3D('',#39377,#16683,#16684);
#13881=AXIS2_PLACEMENT_3D('',#39378,#16685,#16686);
#13882=AXIS2_PLACEMENT_3D('',#39379,#16687,#16688);
#13883=AXIS2_PLACEMENT_3D('',#39380,#16689,#16690);
#13884=AXIS2_PLACEMENT_3D('',#39381,#16691,#16692);
#13885=AXIS2_PLACEMENT_3D('',#39382,#16693,#16694);
#13886=AXIS2_PLACEMENT_3D('',#39383,#16695,#16696);
#13887=AXIS2_PLACEMENT_3D('',#39384,#16697,#16698);
#13888=AXIS2_PLACEMENT_3D('',#39385,#16699,#16700);
#13889=AXIS2_PLACEMENT_3D('',#39386,#16701,#16702);
#13890=AXIS2_PLACEMENT_3D('',#39387,#16703,#16704);
#13891=AXIS2_PLACEMENT_3D('',#39388,#16705,#16706);
#13892=AXIS2_PLACEMENT_3D('',#39389,#16707,#16708);
#13893=AXIS2_PLACEMENT_3D('',#39390,#16709,#16710);
#13894=AXIS2_PLACEMENT_3D('',#39391,#16711,#16712);
#13895=AXIS2_PLACEMENT_3D('',#39392,#16713,#16714);
#13896=AXIS2_PLACEMENT_3D('',#39393,#16715,#16716);
#13897=AXIS2_PLACEMENT_3D('',#39394,#16717,#16718);
#13898=AXIS2_PLACEMENT_3D('',#39395,#16719,#16720);
#13899=AXIS2_PLACEMENT_3D('',#39396,#16721,#16722);
#13900=AXIS2_PLACEMENT_3D('',#39397,#16723,#16724);
#13901=AXIS2_PLACEMENT_3D('',#39398,#16725,#16726);
#13902=AXIS2_PLACEMENT_3D('',#39399,#16727,#16728);
#13903=AXIS2_PLACEMENT_3D('',#39400,#16729,#16730);
#13904=AXIS2_PLACEMENT_3D('',#39401,#16731,#16732);
#13905=AXIS2_PLACEMENT_3D('',#39402,#16733,#16734);
#13906=AXIS2_PLACEMENT_3D('',#39403,#16735,#16736);
#13907=AXIS2_PLACEMENT_3D('',#39404,#16737,#16738);
#13908=AXIS2_PLACEMENT_3D('',#39405,#16739,#16740);
#13909=AXIS2_PLACEMENT_3D('',#39406,#16741,#16742);
#13910=AXIS2_PLACEMENT_3D('',#39407,#16743,#16744);
#13911=AXIS2_PLACEMENT_3D('',#39408,#16745,#16746);
#13912=AXIS2_PLACEMENT_3D('',#39409,#16747,#16748);
#13913=AXIS2_PLACEMENT_3D('',#39410,#16749,#16750);
#13914=AXIS2_PLACEMENT_3D('',#39411,#16751,#16752);
#13915=AXIS2_PLACEMENT_3D('',#39412,#16753,#16754);
#13916=AXIS2_PLACEMENT_3D('',#39413,#16755,#16756);
#13917=AXIS2_PLACEMENT_3D('',#39414,#16757,#16758);
#13918=AXIS2_PLACEMENT_3D('',#39415,#16759,#16760);
#13919=AXIS2_PLACEMENT_3D('',#39416,#16761,#16762);
#13920=AXIS2_PLACEMENT_3D('',#39417,#16763,#16764);
#13921=AXIS2_PLACEMENT_3D('',#39418,#16765,#16766);
#13922=AXIS2_PLACEMENT_3D('',#39419,#16767,#16768);
#13923=AXIS2_PLACEMENT_3D('',#39420,#16769,#16770);
#13924=AXIS2_PLACEMENT_3D('',#39421,#16771,#16772);
#13925=AXIS2_PLACEMENT_3D('',#39422,#16773,#16774);
#13926=AXIS2_PLACEMENT_3D('',#39423,#16775,#16776);
#13927=AXIS2_PLACEMENT_3D('',#39424,#16777,#16778);
#13928=AXIS2_PLACEMENT_3D('',#39425,#16779,#16780);
#13929=AXIS2_PLACEMENT_3D('',#39426,#16781,#16782);
#13930=AXIS2_PLACEMENT_3D('',#39427,#16783,#16784);
#13931=AXIS2_PLACEMENT_3D('',#39428,#16785,#16786);
#13932=AXIS2_PLACEMENT_3D('',#39429,#16787,#16788);
#13933=AXIS2_PLACEMENT_3D('',#39430,#16789,#16790);
#13934=AXIS2_PLACEMENT_3D('',#39431,#16791,#16792);
#13935=AXIS2_PLACEMENT_3D('',#39432,#16793,#16794);
#13936=AXIS2_PLACEMENT_3D('',#39433,#16795,#16796);
#13937=AXIS2_PLACEMENT_3D('',#39434,#16797,#16798);
#13938=AXIS2_PLACEMENT_3D('',#39435,#16799,#16800);
#13939=AXIS2_PLACEMENT_3D('',#39436,#16801,#16802);
#16163=DIRECTION('axis',(0.,0.,1.));
#16164=DIRECTION('refdir',(1.,0.,0.));
#16165=DIRECTION('center_axis',(0.,-1.83697019872103E-16,1.));
#16166=DIRECTION('ref_axis',(0.,-1.,-1.83697019872103E-16));
#16167=DIRECTION('center_axis',(0.,-1.83697019872103E-16,1.));
#16168=DIRECTION('ref_axis',(0.,-1.,-1.83697019872103E-16));
#16169=DIRECTION('center_axis',(1.,1.22464679914735E-16,2.24963967399279E-32));
#16170=DIRECTION('ref_axis',(-1.22464679914735E-16,1.,1.83697019872103E-16));
#16171=DIRECTION('center_axis',(0.,-1.83697019872103E-16,1.));
#16172=DIRECTION('ref_axis',(0.,-1.,-1.83697019872103E-16));
#16173=DIRECTION('center_axis',(0.,1.83697019872103E-16,-1.));
#16174=DIRECTION('ref_axis',(0.,1.,2.09599627067876E-16));
#16175=DIRECTION('center_axis',(0.,1.83697019872103E-16,-1.));
#16176=DIRECTION('ref_axis',(0.,1.,1.83697019872103E-16));
#16177=DIRECTION('center_axis',(0.,1.83697019872103E-16,-1.));
#16178=DIRECTION('ref_axis',(0.,1.,1.83697019872103E-16));
#16179=DIRECTION('center_axis',(-1.,1.22464679914735E-16,2.24963967399279E-32));
#16180=DIRECTION('ref_axis',(-1.22464679914735E-16,-1.,-1.30999766917423E-16));
#16181=DIRECTION('center_axis',(0.,-1.83697019872103E-16,1.));
#16182=DIRECTION('ref_axis',(0.,1.,1.83697019872103E-16));
#16183=DIRECTION('center_axis',(0.,-1.83697019872103E-16,1.));
#16184=DIRECTION('ref_axis',(0.,1.,1.83697019872103E-16));
#16185=DIRECTION('center_axis',(0.,1.83697019872103E-16,-1.));
#16186=DIRECTION('ref_axis',(0.,1.,2.09599627067876E-16));
#16187=DIRECTION('center_axis',(0.,1.83697019872103E-16,-1.));
#16188=DIRECTION('ref_axis',(0.,1.,1.83697019872103E-16));
#16189=DIRECTION('center_axis',(0.,1.83697019872103E-16,-1.));
#16190=DIRECTION('ref_axis',(0.,1.,1.83697019872103E-16));
#16191=DIRECTION('center_axis',(-1.,1.22464679914735E-16,2.24963967399279E-32));
#16192=DIRECTION('ref_axis',(-1.22464679914735E-16,-1.,-1.30999766917423E-16));
#16193=DIRECTION('center_axis',(0.,-1.83697019872103E-16,1.));
#16194=DIRECTION('ref_axis',(0.,-1.,-1.83697019872103E-16));
#16195=DIRECTION('center_axis',(0.,-1.83697019872103E-16,1.));
#16196=DIRECTION('ref_axis',(0.,-1.,-1.83697019872103E-16));
#16197=DIRECTION('',(-8.65956056235483E-17,0.707106781186539,0.707106781186556));
#16198=DIRECTION('center_axis',(0.,-1.83697019872103E-16,1.));
#16199=DIRECTION('ref_axis',(0.,-1.,-1.83697019872103E-16));
#16200=DIRECTION('center_axis',(0.,-1.83697019872103E-16,1.));
#16201=DIRECTION('ref_axis',(0.,-1.,-1.83697019872103E-16));
#16202=DIRECTION('',(0.,-1.83697019872103E-16,1.));
#16203=DIRECTION('center_axis',(0.,1.83697019872103E-16,-1.));
#16204=DIRECTION('ref_axis',(0.,1.,1.83697019872103E-16));
#16205=DIRECTION('',(-8.65956056235483E-17,-0.707106781186539,-0.707106781186556));
#16206=DIRECTION('center_axis',(0.,-1.83697019872103E-16,1.));
#16207=DIRECTION('ref_axis',(0.,-1.,-1.83697019872103E-16));
#16208=DIRECTION('center_axis',(0.,-1.83697019872103E-16,1.));
#16209=DIRECTION('ref_axis',(0.,-1.,-1.83697019872103E-16));
#16210=DIRECTION('',(0.,1.83697019872103E-16,-1.));
#16211=DIRECTION('center_axis',(0.,-1.83697019872103E-16,1.));
#16212=DIRECTION('ref_axis',(0.,-1.,-1.83697019872103E-16));
#16213=DIRECTION('center_axis',(0.,-1.83697019872103E-16,1.));
#16214=DIRECTION('ref_axis',(0.,-1.,-1.83697019872103E-16));
#16215=DIRECTION('center_axis',(0.,-1.83697019872103E-16,1.));
#16216=DIRECTION('ref_axis',(0.,-1.,-1.83697019872103E-16));
#16217=DIRECTION('',(0.,1.83697019872103E-16,-1.));
#16218=DIRECTION('center_axis',(0.,1.83697019872103E-16,-1.));
#16219=DIRECTION('ref_axis',(0.,1.,1.83697019872103E-16));
#16220=DIRECTION('center_axis',(0.,-1.83697019872103E-16,1.));
#16221=DIRECTION('ref_axis',(0.,-1.,-1.83697019872103E-16));
#16222=DIRECTION('center_axis',(-1.,0.,0.));
#16223=DIRECTION('ref_axis',(0.,1.,0.));
#16224=DIRECTION('center_axis',(0.,1.22464679914735E-16,1.));
#16225=DIRECTION('ref_axis',(0.,-1.,1.22464679914735E-16));
#16226=DIRECTION('center_axis',(-0.623489801858732,0.781831482468031,1.43620113371566E-16));
#16227=DIRECTION('ref_axis',(0.781831482468031,0.623489801858732,-6.91638013500061E-17));
#16228=DIRECTION('center_axis',(2.39366855619276E-16,7.19167766472515E-18,
1.));
#16229=DIRECTION('ref_axis',(-0.781831482468031,-0.623489801858732,1.91628481264741E-16));
#16230=DIRECTION('center_axis',(0.222520933956319,0.974927912181823,1.79091352057932E-16));
#16231=DIRECTION('ref_axis',(0.974927912181823,-0.222520933956319,-2.24573452299036E-16));
#16232=DIRECTION('center_axis',(2.98485586763221E-16,-2.51824407250324E-16,
1.));
#16233=DIRECTION('ref_axis',(-0.974927912181823,0.222520933956319,3.47038132213772E-16));
#16234=DIRECTION('center_axis',(0.900968867902422,0.433883739117552,7.97031498468594E-17));
#16235=DIRECTION('ref_axis',(0.433883739117552,-0.900968867902422,-3.4920231590332E-16));
#16236=DIRECTION('center_axis',(1.32838583078098E-16,-4.59539179924132E-16,
1.));
#16237=DIRECTION('ref_axis',(-0.433883739117552,0.900968867902422,4.71666995818055E-16));
#16238=DIRECTION('center_axis',(0.900968867902416,-0.433883739117565,-7.97031498468616E-17));
#16239=DIRECTION('ref_axis',(-0.433883739117565,-0.900968867902416,-3.49202315903319E-16));
#16240=DIRECTION('center_axis',(-1.32838583078103E-16,-4.5953917992413E-16,
1.));
#16241=DIRECTION('ref_axis',(0.433883739117565,0.900968867902416,4.71666995818054E-16));
#16242=DIRECTION('center_axis',(0.222520933956305,-0.974927912181826,-1.79091352057933E-16));
#16243=DIRECTION('ref_axis',(-0.974927912181826,-0.222520933956305,-2.24573452299033E-16));
#16244=DIRECTION('center_axis',(-2.98485586763221E-16,-2.5182440725032E-16,
1.));
#16245=DIRECTION('ref_axis',(0.974927912181826,0.222520933956305,3.47038132213768E-16));
#16246=DIRECTION('center_axis',(-0.623489801858743,-0.781831482468022,-1.43620113371564E-16));
#16247=DIRECTION('ref_axis',(-0.781831482468022,0.623489801858743,-6.91638013500039E-17));
#16248=DIRECTION('center_axis',(-2.39366855619273E-16,7.19167766472869E-18,
1.));
#16249=DIRECTION('ref_axis',(0.781831482468022,-0.623489801858743,1.91628481264739E-16));
#16250=DIRECTION('center_axis',(0.,1.83697019872103E-16,-1.));
#16251=DIRECTION('ref_axis',(0.,1.,1.62614292875575E-16));
#16252=DIRECTION('center_axis',(0.,1.83697019872103E-16,-1.));
#16253=DIRECTION('ref_axis',(0.,1.,1.83697019872103E-16));
#16254=DIRECTION('center_axis',(-1.,1.22464679914735E-16,2.24963967399279E-32));
#16255=DIRECTION('ref_axis',(-1.22464679914735E-16,-1.,-2.03267866094469E-16));
#16256=DIRECTION('center_axis',(0.,-1.83697019872103E-16,1.));
#16257=DIRECTION('ref_axis',(0.,1.,1.83697019872103E-16));
#16258=DIRECTION('center_axis',(0.,-1.83697019872103E-16,1.));
#16259=DIRECTION('ref_axis',(0.,1.,1.83697019872103E-16));
#16260=DIRECTION('center_axis',(0.,-1.83697019872103E-16,1.));
#16261=DIRECTION('ref_axis',(0.,-1.,-1.64970202400831E-16));
#16262=DIRECTION('center_axis',(0.,-1.83697019872103E-16,1.));
#16263=DIRECTION('ref_axis',(0.,-1.,-1.83697019872103E-16));
#16264=DIRECTION('center_axis',(-1.,-1.22464679914735E-16,-2.24963967399279E-32));
#16265=DIRECTION('ref_axis',(-1.22464679914735E-16,1.,2.06212753001039E-16));
#16266=DIRECTION('center_axis',(0.,1.83697019872103E-16,-1.));
#16267=DIRECTION('ref_axis',(0.,-1.,-1.83697019872103E-16));
#16268=DIRECTION('center_axis',(0.,-1.83697019872103E-16,1.));
#16269=DIRECTION('ref_axis',(0.,-1.,-1.62614292875575E-16));
#16270=DIRECTION('center_axis',(0.,-1.83697019872103E-16,1.));
#16271=DIRECTION('ref_axis',(0.,-1.,-1.83697019872103E-16));
#16272=DIRECTION('center_axis',(-1.,-1.22464679914735E-16,-2.24963967399279E-32));
#16273=DIRECTION('ref_axis',(-1.22464679914735E-16,1.,2.03267866094469E-16));
#16274=DIRECTION('center_axis',(0.,1.83697019872103E-16,-1.));
#16275=DIRECTION('ref_axis',(0.,-1.,-1.83697019872103E-16));
#16276=DIRECTION('center_axis',(0.,1.83697019872103E-16,-1.));
#16277=DIRECTION('ref_axis',(0.,1.,1.64970202400831E-16));
#16278=DIRECTION('center_axis',(0.,1.83697019872103E-16,-1.));
#16279=DIRECTION('ref_axis',(0.,1.,1.83697019872103E-16));
#16280=DIRECTION('center_axis',(0.,1.83697019872103E-16,-1.));
#16281=DIRECTION('ref_axis',(0.,1.,1.83697019872103E-16));
#16282=DIRECTION('center_axis',(-1.,1.22464679914735E-16,2.24963967399279E-32));
#16283=DIRECTION('ref_axis',(-1.22464679914735E-16,-1.,-2.06212753001039E-16));
#16284=DIRECTION('center_axis',(0.,-1.83697019872103E-16,1.));
#16285=DIRECTION('ref_axis',(0.,1.,1.83697019872103E-16));
#16286=DIRECTION('center_axis',(0.,-1.83697019872103E-16,1.));
#16287=DIRECTION('ref_axis',(0.,-1.,-1.83697019872103E-16));
#16288=DIRECTION('center_axis',(0.,-1.83697019872103E-16,1.));
#16289=DIRECTION('ref_axis',(0.,-1.,-1.83697019872103E-16));
#16290=DIRECTION('',(0.,-1.83697019872103E-16,1.));
#16291=DIRECTION('center_axis',(0.,-1.83697019872103E-16,1.));
#16292=DIRECTION('ref_axis',(0.,-1.,-1.83697019872103E-16));
#16293=DIRECTION('center_axis',(0.,-1.83697019872103E-16,1.));
#16294=DIRECTION('ref_axis',(0.,-1.,-1.83697019872103E-16));
#16295=DIRECTION('center_axis',(0.,-1.83697019872103E-16,1.));
#16296=DIRECTION('ref_axis',(0.,-1.,-1.83697019872103E-16));
#16297=DIRECTION('',(0.,-1.83697019872103E-16,1.));
#16298=DIRECTION('center_axis',(0.,-1.83697019872103E-16,1.));
#16299=DIRECTION('ref_axis',(0.,-1.,-1.83697019872103E-16));
#16300=DIRECTION('',(0.,-1.83697019872103E-16,1.));
#16301=DIRECTION('center_axis',(0.,-1.83697019872103E-16,1.));
#16302=DIRECTION('ref_axis',(0.,-1.,-1.83697019872103E-16));
#16303=DIRECTION('center_axis',(0.,-1.83697019872103E-16,1.));
#16304=DIRECTION('ref_axis',(0.,-1.,-1.83697019872103E-16));
#16305=DIRECTION('center_axis',(1.,1.22464679914735E-16,2.24963967399279E-32));
#16306=DIRECTION('ref_axis',(-1.22464679914735E-16,1.,1.83697019872103E-16));
#16307=DIRECTION('center_axis',(0.,-1.83697019872103E-16,1.));
#16308=DIRECTION('ref_axis',(0.,-1.,-1.83697019872103E-16));
#16309=DIRECTION('center_axis',(0.,-1.83697019872103E-16,1.));
#16310=DIRECTION('ref_axis',(0.,-1.,-1.83697019872103E-16));
#16311=DIRECTION('',(0.,-1.83697019872103E-16,1.));
#16312=DIRECTION('center_axis',(0.,-1.83697019872103E-16,1.));
#16313=DIRECTION('ref_axis',(0.,-1.,-1.83697019872103E-16));
#16314=DIRECTION('',(0.,-1.83697019872103E-16,1.));
#16315=DIRECTION('center_axis',(0.,-1.83697019872103E-16,1.));
#16316=DIRECTION('ref_axis',(0.,-1.,-1.83697019872103E-16));
#16317=DIRECTION('center_axis',(0.,-1.83697019872103E-16,1.));
#16318=DIRECTION('ref_axis',(0.,-1.,-1.83697019872103E-16));
#16319=DIRECTION('center_axis',(0.,-1.83697019872103E-16,1.));
#16320=DIRECTION('ref_axis',(0.,-1.,-1.83697019872103E-16));
#16321=DIRECTION('',(0.,-1.83697019872103E-16,1.));
#16322=DIRECTION('center_axis',(0.,-1.83697019872103E-16,1.));
#16323=DIRECTION('ref_axis',(0.,-1.,-1.83697019872103E-16));
#16324=DIRECTION('center_axis',(0.,-1.83697019872103E-16,1.));
#16325=DIRECTION('ref_axis',(0.,-1.,-1.83697019872103E-16));
#16326=DIRECTION('center_axis',(0.,-1.83697019872103E-16,1.));
#16327=DIRECTION('ref_axis',(0.,-1.,-1.83697019872103E-16));
#16328=DIRECTION('',(8.65956056235488E-17,-0.707106781186543,-0.707106781186552));
#16329=DIRECTION('center_axis',(0.,-1.83697019872103E-16,1.));
#16330=DIRECTION('ref_axis',(0.,-1.,-1.83697019872103E-16));
#16331=DIRECTION('center_axis',(0.,1.83697019872103E-16,-1.));
#16332=DIRECTION('ref_axis',(0.,1.,1.83697019872103E-16));
#16333=DIRECTION('center_axis',(0.,-1.83697019872103E-16,1.));
#16334=DIRECTION('ref_axis',(0.,-1.,-1.83697019872103E-16));
#16335=DIRECTION('',(8.65956056235488E-17,0.707106781186543,0.707106781186552));
#16336=DIRECTION('center_axis',(0.,-1.83697019872103E-16,1.));
#16337=DIRECTION('ref_axis',(0.,-1.,-1.83697019872103E-16));
#16338=DIRECTION('center_axis',(0.,-1.83697019872103E-16,1.));
#16339=DIRECTION('ref_axis',(0.,-1.,-1.83697019872103E-16));
#16340=DIRECTION('center_axis',(0.,-1.83697019872103E-16,1.));
#16341=DIRECTION('ref_axis',(0.,-1.,-1.83697019872103E-16));
#16342=DIRECTION('',(0.,1.83697019872103E-16,-1.));
#16343=DIRECTION('center_axis',(0.,1.83697019872103E-16,-1.));
#16344=DIRECTION('ref_axis',(0.,1.,1.83697019872103E-16));
#16345=DIRECTION('center_axis',(0.,-1.83697019872103E-16,1.));
#16346=DIRECTION('ref_axis',(0.,-1.,-1.83697019872103E-16));
#16347=DIRECTION('center_axis',(0.,1.83697019872103E-16,-1.));
#16348=DIRECTION('ref_axis',(0.,1.,1.83697019872103E-16));
#16349=DIRECTION('center_axis',(0.,-1.83697019872103E-16,1.));
#16350=DIRECTION('ref_axis',(0.,-1.,-1.83697019872103E-16));
#16351=DIRECTION('center_axis',(0.,1.83697019872103E-16,-1.));
#16352=DIRECTION('ref_axis',(0.,1.,1.83697019872103E-16));
#16353=DIRECTION('center_axis',(0.,-1.83697019872103E-16,1.));
#16354=DIRECTION('ref_axis',(0.,-1.,-1.83697019872103E-16));
#16355=DIRECTION('center_axis',(-0.781831482468031,0.623489801858732,-6.91638013500059E-17));
#16356=DIRECTION('ref_axis',(0.,0.,1.));
#16357=DIRECTION('center_axis',(-0.781831482468031,0.623489801858732,-6.91638013500059E-17));
#16358=DIRECTION('ref_axis',(-5.40744373425995E-17,4.31229247995119E-17,
1.));
#16359=DIRECTION('center_axis',(-0.623489801858732,-0.781831482468031,2.05955304247937E-16));
#16360=DIRECTION('ref_axis',(0.,-2.63426721571497E-16,-1.));
#16361=DIRECTION('center_axis',(-0.781831482468031,0.623489801858732,-6.91638013500059E-17));
#16362=DIRECTION('ref_axis',(-5.40744373425995E-17,4.31229247995119E-17,
1.));
#16363=DIRECTION('center_axis',(0.623489801858732,0.781831482468031,1.22464679914735E-16));
#16364=DIRECTION('ref_axis',(0.,0.,1.));
#16365=DIRECTION('center_axis',(-1.79091352057932E-16,-2.24573452299036E-16,
1.));
#16366=DIRECTION('ref_axis',(-5.50003967499518E-33,-1.,-2.24573452299036E-16));
#16367=DIRECTION('center_axis',(0.781831482468031,-0.623489801858732,0.));
#16368=DIRECTION('ref_axis',(0.,0.,-1.));
#16369=DIRECTION('center_axis',(-1.43620113371566E-16,-6.91638013500059E-17,
1.));
#16370=DIRECTION('ref_axis',(0.623489801858732,0.781831482468031,1.43620113371566E-16));
#16371=DIRECTION('center_axis',(-1.43620113371566E-16,-6.91638013500059E-17,
1.));
#16372=DIRECTION('ref_axis',(0.623489801858732,0.781831482468031,1.43620113371566E-16));
#16373=DIRECTION('center_axis',(-1.43620113371566E-16,-6.91638013500059E-17,
1.));
#16374=DIRECTION('ref_axis',(0.623489801858732,0.781831482468031,1.43620113371566E-16));
#16375=DIRECTION('center_axis',(-1.79091352057932E-16,-2.24573452299036E-16,
1.));
#16376=DIRECTION('ref_axis',(-5.50003967499518E-33,-1.,-2.24573452299036E-16));
#16377=DIRECTION('center_axis',(-1.79091352057932E-16,-2.24573452299036E-16,
1.));
#16378=DIRECTION('ref_axis',(-5.5000396749952E-33,-1.,-2.24573452299036E-16));
#16379=DIRECTION('center_axis',(-0.781831482468031,0.623489801858732,-6.91638013500059E-17));
#16380=DIRECTION('ref_axis',(-5.40744373425995E-17,4.31229247995119E-17,
1.));
#16381=DIRECTION('center_axis',(-0.781831482468031,0.623489801858732,-6.91638013500059E-17));
#16382=DIRECTION('ref_axis',(-5.40744373425995E-17,4.31229247995119E-17,
1.));
#16383=DIRECTION('center_axis',(-0.974927912181823,-0.222520933956318,-2.24573452299036E-16));
#16384=DIRECTION('ref_axis',(0.,-2.10741377257197E-16,1.));
#16385=DIRECTION('center_axis',(-0.974927912181823,-0.222520933956318,-2.24573452299036E-16));
#16386=DIRECTION('ref_axis',(-1.71433215598957E-16,-2.58125940401653E-16,
1.));
#16387=DIRECTION('center_axis',(0.222520933956318,-0.974927912181823,-1.28411031837301E-16));
#16388=DIRECTION('ref_axis',(0.,1.31713360785748E-16,-1.));
#16389=DIRECTION('center_axis',(-0.974927912181823,-0.222520933956318,-2.24573452299036E-16));
#16390=DIRECTION('ref_axis',(-1.71433215598957E-16,-2.58125940401653E-16,
1.));
#16391=DIRECTION('center_axis',(-0.222520933956318,0.974927912181823,3.59586625308286E-16));
#16392=DIRECTION('ref_axis',(0.,-2.4905725751517E-16,1.));
#16393=DIRECTION('center_axis',(-7.97031498468594E-17,-3.4920231590332E-16,
1.));
#16394=DIRECTION('ref_axis',(2.39882519785021E-33,-1.,-3.4920231590332E-16));
#16395=DIRECTION('center_axis',(0.974927912181823,0.222520933956318,6.92755669385935E-17));
#16396=DIRECTION('ref_axis',(0.,3.11321571893962E-16,-1.));
#16397=DIRECTION('center_axis',(-1.79091352057932E-16,-2.24573452299036E-16,
1.));
#16398=DIRECTION('ref_axis',(-0.222520933956318,0.974927912181823,1.79091352057933E-16));
#16399=DIRECTION('center_axis',(-1.79091352057932E-16,-2.24573452299036E-16,
1.));
#16400=DIRECTION('ref_axis',(-0.222520933956318,0.974927912181823,1.79091352057933E-16));
#16401=DIRECTION('center_axis',(-1.79091352057932E-16,-2.24573452299036E-16,
1.));
#16402=DIRECTION('ref_axis',(-0.222520933956318,0.974927912181823,1.79091352057933E-16));
#16403=DIRECTION('center_axis',(-7.97031498468594E-17,-3.4920231590332E-16,
1.));
#16404=DIRECTION('ref_axis',(2.39882519785021E-33,-1.,-3.4920231590332E-16));
#16405=DIRECTION('center_axis',(-7.97031498468594E-17,-3.4920231590332E-16,
1.));
#16406=DIRECTION('ref_axis',(2.39882519785021E-33,-1.,-3.4920231590332E-16));
#16407=DIRECTION('center_axis',(-0.974927912181823,-0.222520933956318,-2.24573452299036E-16));
#16408=DIRECTION('ref_axis',(-1.64444757441796E-16,-2.88744376156862E-16,
1.));
#16409=DIRECTION('center_axis',(-0.974927912181823,-0.222520933956318,-2.24573452299036E-16));
#16410=DIRECTION('ref_axis',(-1.64444757441796E-16,-2.88744376156862E-16,
1.));
#16411=DIRECTION('center_axis',(-0.433883739117553,-0.900968867902422,-3.4920231590332E-16));
#16412=DIRECTION('ref_axis',(0.,-4.21482754514395E-16,1.));
#16413=DIRECTION('center_axis',(-0.433883739117553,-0.900968867902422,-3.4920231590332E-16));
#16414=DIRECTION('ref_axis',(1.97058769816641E-17,-3.97075180104293E-16,
1.));
#16415=DIRECTION('center_axis',(0.900968867902422,-0.433883739117553,-2.28593141877839E-16));
#16416=DIRECTION('ref_axis',(0.,5.26853443142994E-16,-1.));
#16417=DIRECTION('center_axis',(-0.433883739117553,-0.900968867902422,-3.4920231590332E-16));
#16418=DIRECTION('ref_axis',(1.97058769816641E-17,-3.97075180104293E-16,
1.));
#16419=DIRECTION('center_axis',(-0.900968867902422,0.433883739117552,3.33523066916777E-16));
#16420=DIRECTION('ref_axis',(0.,-4.9811451503034E-16,1.));
#16421=DIRECTION('center_axis',(7.97031498468617E-17,-3.49202315903319E-16,
1.));
#16422=DIRECTION('ref_axis',(-2.39882519785018E-33,-1.,-3.49202315903319E-16));
#16423=DIRECTION('center_axis',(0.433883739117552,0.900968867902422,5.60982088365811E-16));
#16424=DIRECTION('ref_axis',(0.,6.22643143787925E-16,-1.));
#16425=DIRECTION('center_axis',(-7.97031498468594E-17,-3.4920231590332E-16,
1.));
#16426=DIRECTION('ref_axis',(-0.900968867902422,0.433883739117553,7.97031498468594E-17));
#16427=DIRECTION('center_axis',(-7.97031498468594E-17,-3.4920231590332E-16,
1.));
#16428=DIRECTION('ref_axis',(-0.900968867902422,0.433883739117553,7.97031498468594E-17));
#16429=DIRECTION('center_axis',(-7.97031498468594E-17,-3.4920231590332E-16,
1.));
#16430=DIRECTION('ref_axis',(-0.900968867902422,0.433883739117553,7.97031498468594E-17));
#16431=DIRECTION('center_axis',(7.97031498468617E-17,-3.49202315903319E-16,
1.));
#16432=DIRECTION('ref_axis',(-2.39882519785018E-33,-1.,-3.49202315903319E-16));
#16433=DIRECTION('center_axis',(7.97031498468617E-17,-3.49202315903319E-16,
1.));
#16434=DIRECTION('ref_axis',(-2.39882519785018E-33,-1.,-3.49202315903319E-16));
#16435=DIRECTION('center_axis',(-0.433883739117553,-0.900968867902422,-3.4920231590332E-16));
#16436=DIRECTION('ref_axis',(4.4891409918625E-17,-4.09203893527874E-16,
1.));
#16437=DIRECTION('center_axis',(-0.433883739117553,-0.900968867902422,-3.4920231590332E-16));
#16438=DIRECTION('ref_axis',(4.48914099186251E-17,-4.09203893527874E-16,
1.));
#16439=DIRECTION('center_axis',(0.433883739117565,-0.900968867902416,-3.49202315903319E-16));
#16440=DIRECTION('ref_axis',(0.,-4.21482754514395E-16,1.));
#16441=DIRECTION('center_axis',(0.433883739117565,-0.900968867902416,-3.49202315903319E-16));
#16442=DIRECTION('ref_axis',(-1.97058769816642E-17,-3.97075180104295E-16,
1.));
#16443=DIRECTION('center_axis',(0.900968867902416,0.433883739117565,2.28593141877845E-16));
#16444=DIRECTION('ref_axis',(0.,5.26853443142994E-16,-1.));
#16445=DIRECTION('center_axis',(0.433883739117565,-0.900968867902416,-3.49202315903319E-16));
#16446=DIRECTION('ref_axis',(-1.97058769816642E-17,-3.97075180104295E-16,
1.));
#16447=DIRECTION('center_axis',(-0.900968867902416,-0.433883739117565,-8.85937070873124E-17));
#16448=DIRECTION('ref_axis',(0.,-4.9811451503034E-16,1.));
#16449=DIRECTION('center_axis',(1.79091352057933E-16,-2.24573452299033E-16,
1.));
#16450=DIRECTION('ref_axis',(5.50003967499563E-33,-1.,-2.24573452299033E-16));
#16451=DIRECTION('center_axis',(-0.433883739117565,0.900968867902416,5.60982088365808E-16));
#16452=DIRECTION('ref_axis',(0.,6.22643143787925E-16,-1.));
#16453=DIRECTION('center_axis',(7.97031498468617E-17,-3.49202315903319E-16,
1.));
#16454=DIRECTION('ref_axis',(-0.900968867902416,-0.433883739117565,-7.97031498468616E-17));
#16455=DIRECTION('center_axis',(7.97031498468617E-17,-3.49202315903319E-16,
1.));
#16456=DIRECTION('ref_axis',(-0.900968867902416,-0.433883739117565,-7.97031498468616E-17));
#16457=DIRECTION('center_axis',(7.97031498468617E-17,-3.49202315903319E-16,
1.));
#16458=DIRECTION('ref_axis',(-0.900968867902416,-0.433883739117565,-7.97031498468616E-17));
#16459=DIRECTION('center_axis',(1.79091352057933E-16,-2.24573452299033E-16,
1.));
#16460=DIRECTION('ref_axis',(5.50003967499563E-33,-1.,-2.24573452299033E-16));
#16461=DIRECTION('center_axis',(1.79091352057933E-16,-2.24573452299033E-16,
1.));
#16462=DIRECTION('ref_axis',(5.50003967499563E-33,-1.,-2.24573452299033E-16));
#16463=DIRECTION('center_axis',(0.433883739117565,-0.900968867902416,-3.49202315903319E-16));
#16464=DIRECTION('ref_axis',(-4.48914099186257E-17,-4.09203893527877E-16,
1.));
#16465=DIRECTION('center_axis',(0.433883739117565,-0.900968867902416,-3.49202315903319E-16));
#16466=DIRECTION('ref_axis',(-4.48914099186258E-17,-4.09203893527877E-16,
1.));
#16467=DIRECTION('center_axis',(0.974927912181826,-0.222520933956305,-2.24573452299033E-16));
#16468=DIRECTION('ref_axis',(0.,-2.10741377257197E-16,1.));
#16469=DIRECTION('center_axis',(0.974927912181826,-0.222520933956305,-2.24573452299033E-16));
#16470=DIRECTION('ref_axis',(1.71433215598957E-16,-2.58125940401651E-16,
1.));
#16471=DIRECTION('center_axis',(0.222520933956305,0.974927912181826,3.85233095511904E-16));
#16472=DIRECTION('ref_axis',(0.,3.95140082357245E-16,-1.));
#16473=DIRECTION('center_axis',(0.974927912181826,-0.222520933956305,-2.24573452299033E-16));
#16474=DIRECTION('ref_axis',(1.71433215598957E-16,-2.58125940401651E-16,
1.));
#16475=DIRECTION('center_axis',(-0.222520933956305,-0.974927912181826,-1.14657265478815E-16));
#16476=DIRECTION('ref_axis',(0.,-1.24528628757585E-16,1.));
#16477=DIRECTION('center_axis',(1.43620113371564E-16,-6.91638013500039E-17,
1.));
#16478=DIRECTION('ref_axis',(1.,1.10509814492259E-33,-1.43620113371564E-16));
#16479=DIRECTION('center_axis',(-0.974927912181826,0.222520933956305,3.46377834692947E-17));
#16480=DIRECTION('ref_axis',(0.,1.55660785946981E-16,-1.));
#16481=DIRECTION('center_axis',(1.79091352057933E-16,-2.24573452299033E-16,
1.));
#16482=DIRECTION('ref_axis',(-0.222520933956305,-0.974927912181826,-1.79091352057932E-16));
#16483=DIRECTION('center_axis',(1.79091352057933E-16,-2.24573452299033E-16,
1.));
#16484=DIRECTION('ref_axis',(-0.222520933956305,-0.974927912181826,-1.79091352057932E-16));
#16485=DIRECTION('center_axis',(1.79091352057933E-16,-2.24573452299033E-16,
1.));
#16486=DIRECTION('ref_axis',(-0.222520933956305,-0.974927912181826,-1.79091352057932E-16));
#16487=DIRECTION('center_axis',(1.43620113371564E-16,-6.91638013500039E-17,
1.));
#16488=DIRECTION('ref_axis',(1.,1.10509814492259E-33,-1.43620113371564E-16));
#16489=DIRECTION('center_axis',(1.43620113371564E-16,-6.91638013500039E-17,
1.));
#16490=DIRECTION('ref_axis',(1.,1.10509814492259E-33,-1.43620113371564E-16));
#16491=DIRECTION('center_axis',(0.974927912181826,-0.222520933956305,-2.24573452299033E-16));
#16492=DIRECTION('ref_axis',(1.64444757441797E-16,-2.8874437615686E-16,
1.));
#16493=DIRECTION('center_axis',(0.974927912181826,-0.222520933956305,-2.24573452299033E-16));
#16494=DIRECTION('ref_axis',(1.64444757441797E-16,-2.8874437615686E-16,
1.));
#16495=DIRECTION('center_axis',(0.781831482468022,0.623489801858743,-6.91638013500039E-17));
#16496=DIRECTION('ref_axis',(0.,0.,1.));
#16497=DIRECTION('center_axis',(0.781831482468022,0.623489801858743,-6.91638013500039E-17));
#16498=DIRECTION('ref_axis',(5.40744373425973E-17,4.31229247995114E-17,
1.));
#16499=DIRECTION('center_axis',(-0.623489801858743,0.781831482468022,0.));
#16500=DIRECTION('ref_axis',(0.,0.,-1.));
#16501=DIRECTION('center_axis',(0.781831482468022,0.623489801858743,-6.91638013500039E-17));
#16502=DIRECTION('ref_axis',(5.40744373425973E-17,4.31229247995114E-17,
1.));
#16503=DIRECTION('center_axis',(0.623489801858743,-0.781831482468022,1.22464679914735E-16));
#16504=DIRECTION('ref_axis',(0.,0.,1.));
#16505=DIRECTION('center_axis',(0.,0.,-1.));
#16506=DIRECTION('ref_axis',(1.,0.,0.));
#16507=DIRECTION('center_axis',(0.,0.,-1.));
#16508=DIRECTION('ref_axis',(1.,0.,0.));
#16509=DIRECTION('center_axis',(0.,0.,-1.));
#16510=DIRECTION('ref_axis',(1.,0.,0.));
#16511=DIRECTION('center_axis',(-0.781831482468022,-0.623489801858743,0.));
#16512=DIRECTION('ref_axis',(0.,0.,-1.));
#16513=DIRECTION('center_axis',(1.43620113371564E-16,-6.91638013500039E-17,
1.));
#16514=DIRECTION('ref_axis',(0.623489801858743,-0.781831482468022,-1.43620113371564E-16));
#16515=DIRECTION('center_axis',(1.43620113371564E-16,-6.91638013500039E-17,
1.));
#16516=DIRECTION('ref_axis',(0.623489801858743,-0.781831482468022,-1.43620113371564E-16));
#16517=DIRECTION('center_axis',(1.43620113371564E-16,-6.91638013500039E-17,
1.));
#16518=DIRECTION('ref_axis',(0.623489801858743,-0.781831482468022,-1.43620113371564E-16));
#16519=DIRECTION('center_axis',(0.781831482468022,0.623489801858743,-6.91638013500039E-17));
#16520=DIRECTION('ref_axis',(5.40744373425973E-17,4.31229247995114E-17,
1.));
#16521=DIRECTION('center_axis',(0.781831482468022,0.623489801858743,-6.91638013500039E-17));
#16522=DIRECTION('ref_axis',(5.40744373425973E-17,4.31229247995114E-17,
1.));
#16523=DIRECTION('center_axis',(1.,0.,1.22464679914735E-16));
#16524=DIRECTION('ref_axis',(-6.12323399573677E-17,0.,1.));
#16525=DIRECTION('center_axis',(-1.43620113371566E-16,-6.91638013500059E-17,
1.));
#16526=DIRECTION('ref_axis',(1.,-1.10509814492274E-33,1.43620113371566E-16));
#16527=DIRECTION('center_axis',(0.,-1.,0.));
#16528=DIRECTION('ref_axis',(6.12323399573677E-17,0.,-1.));
#16529=DIRECTION('center_axis',(0.,0.,1.));
#16530=DIRECTION('ref_axis',(1.,0.,0.));
#16531=DIRECTION('center_axis',(0.,0.,1.));
#16532=DIRECTION('ref_axis',(1.,0.,0.));
#16533=DIRECTION('center_axis',(0.,0.,1.));
#16534=DIRECTION('ref_axis',(1.,0.,0.));
#16535=DIRECTION('center_axis',(-1.43620113371566E-16,-6.91638013500059E-17,
1.));
#16536=DIRECTION('ref_axis',(1.,-1.10509814492274E-33,1.43620113371566E-16));
#16537=DIRECTION('center_axis',(-1.43620113371566E-16,-6.91638013500059E-17,
1.));
#16538=DIRECTION('ref_axis',(1.,-1.10509814492274E-33,1.43620113371566E-16));
#16539=DIRECTION('center_axis',(0.,1.,0.));
#16540=DIRECTION('ref_axis',(0.,0.,1.));
#16541=DIRECTION('center_axis',(0.,1.,0.));
#16542=DIRECTION('ref_axis',(0.,0.,1.));
#16543=DIRECTION('center_axis',(0.,1.,0.));
#16544=DIRECTION('ref_axis',(0.,0.,1.));
#16545=DIRECTION('center_axis',(0.,1.,0.));
#16546=DIRECTION('ref_axis',(0.,0.,1.));
#16547=DIRECTION('center_axis',(-1.,0.,1.22464679914735E-16));
#16548=DIRECTION('ref_axis',(-1.22464679914735E-16,0.,-1.));
#16549=DIRECTION('center_axis',(0.,1.,0.));
#16550=DIRECTION('ref_axis',(0.,0.,1.));
#16551=DIRECTION('center_axis',(0.,0.,-1.));
#16552=DIRECTION('ref_axis',(-1.,0.,0.));
#16553=DIRECTION('center_axis',(0.,0.,-1.));
#16554=DIRECTION('ref_axis',(1.,0.,0.));
#16555=DIRECTION('center_axis',(0.,0.,-1.));
#16556=DIRECTION('ref_axis',(1.,0.,0.));
#16557=DIRECTION('center_axis',(0.,0.,-1.));
#16558=DIRECTION('ref_axis',(-1.,0.,0.));
#16559=DIRECTION('center_axis',(0.,0.,1.));
#16560=DIRECTION('ref_axis',(1.,0.,0.));
#16561=DIRECTION('center_axis',(0.,0.,1.));
#16562=DIRECTION('ref_axis',(1.,0.,0.));
#16563=DIRECTION('center_axis',(0.,0.,1.));
#16564=DIRECTION('ref_axis',(1.,0.,0.));
#16565=DIRECTION('center_axis',(0.,0.,1.));
#16566=DIRECTION('ref_axis',(1.,0.,0.));
#16567=DIRECTION('center_axis',(0.,1.,0.));
#16568=DIRECTION('ref_axis',(0.,0.,1.));
#16569=DIRECTION('center_axis',(0.,-1.,0.));
#16570=DIRECTION('ref_axis',(0.,0.,-1.));
#16571=DIRECTION('center_axis',(0.,0.,1.));
#16572=DIRECTION('ref_axis',(1.,0.,0.));
#16573=DIRECTION('center_axis',(0.,0.,-1.));
#16574=DIRECTION('ref_axis',(1.,0.,0.));
#16575=DIRECTION('center_axis',(0.,0.,1.));
#16576=DIRECTION('ref_axis',(1.,0.,0.));
#16577=DIRECTION('center_axis',(0.,0.,1.));
#16578=DIRECTION('ref_axis',(1.,0.,0.));
#16579=DIRECTION('center_axis',(0.,0.,-1.));
#16580=DIRECTION('ref_axis',(1.,0.,0.));
#16581=DIRECTION('center_axis',(0.,0.,1.));
#16582=DIRECTION('ref_axis',(1.,0.,0.));
#16583=DIRECTION('center_axis',(0.,0.,-1.));
#16584=DIRECTION('ref_axis',(-1.,0.,0.));
#16585=DIRECTION('center_axis',(0.,0.,-1.));
#16586=DIRECTION('ref_axis',(-1.,0.,0.));
#16587=DIRECTION('center_axis',(-0.781831482468022,-0.623489801858743,6.91638013500039E-17));
#16588=DIRECTION('ref_axis',(-1.43620113371564E-16,6.91638013500039E-17,
-1.));
#16589=DIRECTION('center_axis',(0.781831482468022,0.623489801858743,-6.91638013500039E-17));
#16590=DIRECTION('ref_axis',(1.43620113371564E-16,-6.91638013500039E-17,
1.));
#16591=DIRECTION('center_axis',(1.43620113371564E-16,-6.91638013500039E-17,
1.));
#16592=DIRECTION('ref_axis',(0.623489801858743,-0.781831482468022,-1.43620113371564E-16));
#16593=DIRECTION('center_axis',(-1.43620113371564E-16,6.91638013500039E-17,
-1.));
#16594=DIRECTION('ref_axis',(0.623489801858743,-0.781831482468022,-1.43620113371564E-16));
#16595=DIRECTION('center_axis',(1.43620113371564E-16,-6.91638013500039E-17,
1.));
#16596=DIRECTION('ref_axis',(0.623489801858743,-0.781831482468022,-1.43620113371564E-16));
#16597=DIRECTION('center_axis',(1.43620113371564E-16,-6.91638013500039E-17,
1.));
#16598=DIRECTION('ref_axis',(0.623489801858743,-0.781831482468022,-1.43620113371564E-16));
#16599=DIRECTION('center_axis',(-1.43620113371564E-16,6.91638013500039E-17,
-1.));
#16600=DIRECTION('ref_axis',(0.623489801858743,-0.781831482468022,-1.43620113371564E-16));
#16601=DIRECTION('center_axis',(1.43620113371564E-16,-6.91638013500039E-17,
1.));
#16602=DIRECTION('ref_axis',(0.623489801858743,-0.781831482468022,-1.43620113371564E-16));
#16603=DIRECTION('center_axis',(-1.43620113371564E-16,6.91638013500039E-17,
-1.));
#16604=DIRECTION('ref_axis',(-0.623489801858743,0.781831482468022,1.43620113371564E-16));
#16605=DIRECTION('center_axis',(-1.43620113371564E-16,6.91638013500039E-17,
-1.));
#16606=DIRECTION('ref_axis',(-0.623489801858743,0.781831482468022,1.43620113371564E-16));
#16607=DIRECTION('center_axis',(-1.79091352057933E-16,2.24573452299033E-16,
-1.));
#16608=DIRECTION('ref_axis',(0.222520933956305,0.974927912181826,1.79091352057932E-16));
#16609=DIRECTION('center_axis',(-1.79091352057933E-16,2.24573452299033E-16,
-1.));
#16610=DIRECTION('ref_axis',(-0.222520933956305,-0.974927912181826,-1.79091352057932E-16));
#16611=DIRECTION('center_axis',(-1.79091352057933E-16,2.24573452299033E-16,
-1.));
#16612=DIRECTION('ref_axis',(-0.222520933956305,-0.974927912181826,-1.79091352057932E-16));
#16613=DIRECTION('center_axis',(-1.79091352057933E-16,2.24573452299033E-16,
-1.));
#16614=DIRECTION('ref_axis',(0.222520933956305,0.974927912181826,1.79091352057932E-16));
#16615=DIRECTION('center_axis',(1.79091352057933E-16,-2.24573452299033E-16,
1.));
#16616=DIRECTION('ref_axis',(-0.222520933956305,-0.974927912181826,-1.79091352057932E-16));
#16617=DIRECTION('center_axis',(1.79091352057933E-16,-2.24573452299033E-16,
1.));
#16618=DIRECTION('ref_axis',(-0.222520933956305,-0.974927912181826,-1.79091352057932E-16));
#16619=DIRECTION('center_axis',(1.79091352057933E-16,-2.24573452299033E-16,
1.));
#16620=DIRECTION('ref_axis',(-0.222520933956305,-0.974927912181826,-1.79091352057932E-16));
#16621=DIRECTION('center_axis',(1.79091352057933E-16,-2.24573452299033E-16,
1.));
#16622=DIRECTION('ref_axis',(-0.222520933956305,-0.974927912181826,-1.79091352057932E-16));
#16623=DIRECTION('center_axis',(-0.974927912181826,0.222520933956305,2.24573452299033E-16));
#16624=DIRECTION('ref_axis',(-1.79091352057933E-16,2.24573452299033E-16,
-1.));
#16625=DIRECTION('center_axis',(0.974927912181826,-0.222520933956305,-2.24573452299033E-16));
#16626=DIRECTION('ref_axis',(1.79091352057933E-16,-2.24573452299033E-16,
1.));
#16627=DIRECTION('center_axis',(1.79091352057933E-16,-2.24573452299033E-16,
1.));
#16628=DIRECTION('ref_axis',(-0.222520933956305,-0.974927912181826,-1.79091352057932E-16));
#16629=DIRECTION('center_axis',(-1.79091352057933E-16,2.24573452299033E-16,
-1.));
#16630=DIRECTION('ref_axis',(-0.222520933956305,-0.974927912181826,-1.79091352057932E-16));
#16631=DIRECTION('center_axis',(1.79091352057933E-16,-2.24573452299033E-16,
1.));
#16632=DIRECTION('ref_axis',(-0.222520933956305,-0.974927912181826,-1.79091352057932E-16));
#16633=DIRECTION('center_axis',(1.79091352057933E-16,-2.24573452299033E-16,
1.));
#16634=DIRECTION('ref_axis',(-0.222520933956305,-0.974927912181826,-1.79091352057932E-16));
#16635=DIRECTION('center_axis',(-1.79091352057933E-16,2.24573452299033E-16,
-1.));
#16636=DIRECTION('ref_axis',(-0.222520933956305,-0.974927912181826,-1.79091352057932E-16));
#16637=DIRECTION('center_axis',(1.79091352057933E-16,-2.24573452299033E-16,
1.));
#16638=DIRECTION('ref_axis',(-0.222520933956305,-0.974927912181826,-1.79091352057932E-16));
#16639=DIRECTION('center_axis',(-1.79091352057933E-16,2.24573452299033E-16,
-1.));
#16640=DIRECTION('ref_axis',(0.222520933956305,0.974927912181826,1.79091352057932E-16));
#16641=DIRECTION('center_axis',(-1.79091352057933E-16,2.24573452299033E-16,
-1.));
#16642=DIRECTION('ref_axis',(0.222520933956305,0.974927912181826,1.79091352057932E-16));
#16643=DIRECTION('center_axis',(-7.97031498468617E-17,3.49202315903319E-16,
-1.));
#16644=DIRECTION('ref_axis',(0.900968867902416,0.433883739117565,7.97031498468616E-17));
#16645=DIRECTION('center_axis',(-7.97031498468617E-17,3.49202315903319E-16,
-1.));
#16646=DIRECTION('ref_axis',(-0.900968867902416,-0.433883739117565,-7.97031498468616E-17));
#16647=DIRECTION('center_axis',(-7.97031498468617E-17,3.49202315903319E-16,
-1.));
#16648=DIRECTION('ref_axis',(-0.900968867902416,-0.433883739117565,-7.97031498468616E-17));
#16649=DIRECTION('center_axis',(-7.97031498468617E-17,3.49202315903319E-16,
-1.));
#16650=DIRECTION('ref_axis',(0.900968867902416,0.433883739117565,7.97031498468616E-17));
#16651=DIRECTION('center_axis',(7.97031498468617E-17,-3.49202315903319E-16,
1.));
#16652=DIRECTION('ref_axis',(-0.900968867902416,-0.433883739117565,-7.97031498468616E-17));
#16653=DIRECTION('center_axis',(7.97031498468617E-17,-3.49202315903319E-16,
1.));
#16654=DIRECTION('ref_axis',(-0.900968867902416,-0.433883739117565,-7.97031498468616E-17));
#16655=DIRECTION('center_axis',(7.97031498468617E-17,-3.49202315903319E-16,
1.));
#16656=DIRECTION('ref_axis',(-0.900968867902416,-0.433883739117565,-7.97031498468616E-17));
#16657=DIRECTION('center_axis',(7.97031498468617E-17,-3.49202315903319E-16,
1.));
#16658=DIRECTION('ref_axis',(-0.900968867902416,-0.433883739117565,-7.97031498468616E-17));
#16659=DIRECTION('center_axis',(-0.433883739117565,0.900968867902416,3.49202315903319E-16));
#16660=DIRECTION('ref_axis',(-7.97031498468617E-17,3.49202315903319E-16,
-1.));
#16661=DIRECTION('center_axis',(0.433883739117565,-0.900968867902416,-3.49202315903319E-16));
#16662=DIRECTION('ref_axis',(7.97031498468617E-17,-3.49202315903319E-16,
1.));
#16663=DIRECTION('center_axis',(7.97031498468617E-17,-3.49202315903319E-16,
1.));
#16664=DIRECTION('ref_axis',(-0.900968867902416,-0.433883739117565,-7.97031498468616E-17));
#16665=DIRECTION('center_axis',(-7.97031498468617E-17,3.49202315903319E-16,
-1.));
#16666=DIRECTION('ref_axis',(-0.900968867902416,-0.433883739117565,-7.97031498468616E-17));
#16667=DIRECTION('center_axis',(7.97031498468617E-17,-3.49202315903319E-16,
1.));
#16668=DIRECTION('ref_axis',(-0.900968867902416,-0.433883739117565,-7.97031498468616E-17));
#16669=DIRECTION('center_axis',(7.97031498468617E-17,-3.49202315903319E-16,
1.));
#16670=DIRECTION('ref_axis',(-0.900968867902416,-0.433883739117565,-7.97031498468616E-17));
#16671=DIRECTION('center_axis',(-7.97031498468617E-17,3.49202315903319E-16,
-1.));
#16672=DIRECTION('ref_axis',(-0.900968867902416,-0.433883739117565,-7.97031498468616E-17));
#16673=DIRECTION('center_axis',(7.97031498468617E-17,-3.49202315903319E-16,
1.));
#16674=DIRECTION('ref_axis',(-0.900968867902416,-0.433883739117565,-7.97031498468616E-17));
#16675=DIRECTION('center_axis',(-7.97031498468617E-17,3.49202315903319E-16,
-1.));
#16676=DIRECTION('ref_axis',(0.900968867902416,0.433883739117565,7.97031498468616E-17));
#16677=DIRECTION('center_axis',(-7.97031498468617E-17,3.49202315903319E-16,
-1.));
#16678=DIRECTION('ref_axis',(0.900968867902416,0.433883739117565,7.97031498468616E-17));
#16679=DIRECTION('center_axis',(7.97031498468594E-17,3.4920231590332E-16,
-1.));
#16680=DIRECTION('ref_axis',(0.900968867902422,-0.433883739117553,-7.97031498468594E-17));
#16681=DIRECTION('center_axis',(7.97031498468594E-17,3.4920231590332E-16,
-1.));
#16682=DIRECTION('ref_axis',(-0.900968867902422,0.433883739117553,7.97031498468594E-17));
#16683=DIRECTION('center_axis',(7.97031498468594E-17,3.4920231590332E-16,
-1.));
#16684=DIRECTION('ref_axis',(-0.900968867902422,0.433883739117553,7.97031498468594E-17));
#16685=DIRECTION('center_axis',(7.97031498468594E-17,3.4920231590332E-16,
-1.));
#16686=DIRECTION('ref_axis',(0.900968867902422,-0.433883739117553,-7.97031498468594E-17));
#16687=DIRECTION('center_axis',(-7.97031498468594E-17,-3.4920231590332E-16,
1.));
#16688=DIRECTION('ref_axis',(-0.900968867902422,0.433883739117553,7.97031498468594E-17));
#16689=DIRECTION('center_axis',(-7.97031498468594E-17,-3.4920231590332E-16,
1.));
#16690=DIRECTION('ref_axis',(-0.900968867902422,0.433883739117553,7.97031498468594E-17));
#16691=DIRECTION('center_axis',(-7.97031498468594E-17,-3.4920231590332E-16,
1.));
#16692=DIRECTION('ref_axis',(-0.900968867902422,0.433883739117553,7.97031498468594E-17));
#16693=DIRECTION('center_axis',(-7.97031498468594E-17,-3.4920231590332E-16,
1.));
#16694=DIRECTION('ref_axis',(-0.900968867902422,0.433883739117553,7.97031498468594E-17));
#16695=DIRECTION('center_axis',(0.433883739117553,0.900968867902422,3.4920231590332E-16));
#16696=DIRECTION('ref_axis',(7.97031498468594E-17,3.4920231590332E-16,-1.));
#16697=DIRECTION('center_axis',(-0.433883739117553,-0.900968867902422,-3.4920231590332E-16));
#16698=DIRECTION('ref_axis',(-7.97031498468594E-17,-3.4920231590332E-16,
1.));
#16699=DIRECTION('center_axis',(-7.97031498468594E-17,-3.4920231590332E-16,
1.));
#16700=DIRECTION('ref_axis',(-0.900968867902422,0.433883739117553,7.97031498468594E-17));
#16701=DIRECTION('center_axis',(7.97031498468594E-17,3.4920231590332E-16,
-1.));
#16702=DIRECTION('ref_axis',(-0.900968867902422,0.433883739117553,7.97031498468594E-17));
#16703=DIRECTION('center_axis',(-7.97031498468594E-17,-3.4920231590332E-16,
1.));
#16704=DIRECTION('ref_axis',(-0.900968867902422,0.433883739117553,7.97031498468594E-17));
#16705=DIRECTION('center_axis',(-7.97031498468594E-17,-3.4920231590332E-16,
1.));
#16706=DIRECTION('ref_axis',(-0.900968867902422,0.433883739117553,7.97031498468594E-17));
#16707=DIRECTION('center_axis',(7.97031498468594E-17,3.4920231590332E-16,
-1.));
#16708=DIRECTION('ref_axis',(-0.900968867902422,0.433883739117553,7.97031498468594E-17));
#16709=DIRECTION('center_axis',(-7.97031498468594E-17,-3.4920231590332E-16,
1.));
#16710=DIRECTION('ref_axis',(-0.900968867902422,0.433883739117553,7.97031498468594E-17));
#16711=DIRECTION('center_axis',(7.97031498468594E-17,3.4920231590332E-16,
-1.));
#16712=DIRECTION('ref_axis',(0.900968867902422,-0.433883739117553,-7.97031498468594E-17));
#16713=DIRECTION('center_axis',(7.97031498468594E-17,3.4920231590332E-16,
-1.));
#16714=DIRECTION('ref_axis',(0.900968867902422,-0.433883739117553,-7.97031498468594E-17));
#16715=DIRECTION('center_axis',(1.79091352057932E-16,2.24573452299036E-16,
-1.));
#16716=DIRECTION('ref_axis',(0.222520933956318,-0.974927912181823,-1.79091352057933E-16));
#16717=DIRECTION('center_axis',(1.79091352057932E-16,2.24573452299036E-16,
-1.));
#16718=DIRECTION('ref_axis',(-0.222520933956318,0.974927912181823,1.79091352057933E-16));
#16719=DIRECTION('center_axis',(1.79091352057932E-16,2.24573452299036E-16,
-1.));
#16720=DIRECTION('ref_axis',(-0.222520933956318,0.974927912181823,1.79091352057933E-16));
#16721=DIRECTION('center_axis',(1.79091352057932E-16,2.24573452299036E-16,
-1.));
#16722=DIRECTION('ref_axis',(0.222520933956318,-0.974927912181823,-1.79091352057933E-16));
#16723=DIRECTION('center_axis',(-1.79091352057932E-16,-2.24573452299036E-16,
1.));
#16724=DIRECTION('ref_axis',(-0.222520933956318,0.974927912181823,1.79091352057933E-16));
#16725=DIRECTION('center_axis',(-1.79091352057932E-16,-2.24573452299036E-16,
1.));
#16726=DIRECTION('ref_axis',(-0.222520933956318,0.974927912181823,1.79091352057933E-16));
#16727=DIRECTION('center_axis',(-1.79091352057932E-16,-2.24573452299036E-16,
1.));
#16728=DIRECTION('ref_axis',(-0.222520933956318,0.974927912181823,1.79091352057933E-16));
#16729=DIRECTION('center_axis',(-1.79091352057932E-16,-2.24573452299036E-16,
1.));
#16730=DIRECTION('ref_axis',(-0.222520933956318,0.974927912181823,1.79091352057933E-16));
#16731=DIRECTION('center_axis',(0.974927912181823,0.222520933956318,2.24573452299036E-16));
#16732=DIRECTION('ref_axis',(1.79091352057932E-16,2.24573452299036E-16,
-1.));
#16733=DIRECTION('center_axis',(-0.974927912181823,-0.222520933956318,-2.24573452299036E-16));
#16734=DIRECTION('ref_axis',(-1.79091352057932E-16,-2.24573452299036E-16,
1.));
#16735=DIRECTION('center_axis',(-1.79091352057932E-16,-2.24573452299036E-16,
1.));
#16736=DIRECTION('ref_axis',(-0.222520933956318,0.974927912181823,1.79091352057933E-16));
#16737=DIRECTION('center_axis',(1.79091352057932E-16,2.24573452299036E-16,
-1.));
#16738=DIRECTION('ref_axis',(-0.222520933956318,0.974927912181823,1.79091352057933E-16));
#16739=DIRECTION('center_axis',(-1.79091352057932E-16,-2.24573452299036E-16,
1.));
#16740=DIRECTION('ref_axis',(-0.222520933956318,0.974927912181823,1.79091352057933E-16));
#16741=DIRECTION('center_axis',(-1.79091352057932E-16,-2.24573452299036E-16,
1.));
#16742=DIRECTION('ref_axis',(-0.222520933956318,0.974927912181823,1.79091352057933E-16));
#16743=DIRECTION('center_axis',(1.79091352057932E-16,2.24573452299036E-16,
-1.));
#16744=DIRECTION('ref_axis',(-0.222520933956318,0.974927912181823,1.79091352057933E-16));
#16745=DIRECTION('center_axis',(-1.79091352057932E-16,-2.24573452299036E-16,
1.));
#16746=DIRECTION('ref_axis',(-0.222520933956318,0.974927912181823,1.79091352057933E-16));
#16747=DIRECTION('center_axis',(1.79091352057932E-16,2.24573452299036E-16,
-1.));
#16748=DIRECTION('ref_axis',(0.222520933956318,-0.974927912181823,-1.79091352057933E-16));
#16749=DIRECTION('center_axis',(1.79091352057932E-16,2.24573452299036E-16,
-1.));
#16750=DIRECTION('ref_axis',(0.222520933956318,-0.974927912181823,-1.79091352057933E-16));
#16751=DIRECTION('center_axis',(1.43620113371566E-16,6.91638013500059E-17,
-1.));
#16752=DIRECTION('ref_axis',(-0.623489801858732,-0.781831482468031,-1.43620113371566E-16));
#16753=DIRECTION('center_axis',(1.43620113371566E-16,6.91638013500059E-17,
-1.));
#16754=DIRECTION('ref_axis',(0.623489801858732,0.781831482468031,1.43620113371566E-16));
#16755=DIRECTION('center_axis',(1.43620113371566E-16,6.91638013500059E-17,
-1.));
#16756=DIRECTION('ref_axis',(0.623489801858732,0.781831482468031,1.43620113371566E-16));
#16757=DIRECTION('center_axis',(1.43620113371566E-16,6.91638013500059E-17,
-1.));
#16758=DIRECTION('ref_axis',(-0.623489801858732,-0.781831482468031,-1.43620113371566E-16));
#16759=DIRECTION('center_axis',(-1.43620113371566E-16,-6.91638013500059E-17,
1.));
#16760=DIRECTION('ref_axis',(0.623489801858732,0.781831482468031,1.43620113371566E-16));
#16761=DIRECTION('center_axis',(-1.43620113371566E-16,-6.91638013500059E-17,
1.));
#16762=DIRECTION('ref_axis',(0.623489801858732,0.781831482468031,1.43620113371566E-16));
#16763=DIRECTION('center_axis',(-1.43620113371566E-16,-6.91638013500059E-17,
1.));
#16764=DIRECTION('ref_axis',(0.623489801858732,0.781831482468031,1.43620113371566E-16));
#16765=DIRECTION('center_axis',(-1.43620113371566E-16,-6.91638013500059E-17,
1.));
#16766=DIRECTION('ref_axis',(0.623489801858732,0.781831482468031,1.43620113371566E-16));
#16767=DIRECTION('center_axis',(0.781831482468031,-0.623489801858732,6.91638013500059E-17));
#16768=DIRECTION('ref_axis',(1.43620113371566E-16,6.91638013500061E-17,
-1.));
#16769=DIRECTION('center_axis',(-0.781831482468031,0.623489801858732,-6.91638013500059E-17));
#16770=DIRECTION('ref_axis',(-1.43620113371566E-16,-6.91638013500061E-17,
1.));
#16771=DIRECTION('center_axis',(-1.43620113371566E-16,-6.91638013500059E-17,
1.));
#16772=DIRECTION('ref_axis',(0.623489801858732,0.781831482468031,1.43620113371566E-16));
#16773=DIRECTION('center_axis',(1.43620113371566E-16,6.91638013500059E-17,
-1.));
#16774=DIRECTION('ref_axis',(0.623489801858732,0.781831482468031,1.43620113371566E-16));
#16775=DIRECTION('center_axis',(-1.43620113371566E-16,-6.91638013500059E-17,
1.));
#16776=DIRECTION('ref_axis',(0.623489801858732,0.781831482468031,1.43620113371566E-16));
#16777=DIRECTION('center_axis',(-1.43620113371566E-16,-6.91638013500059E-17,
1.));
#16778=DIRECTION('ref_axis',(0.623489801858732,0.781831482468031,1.43620113371566E-16));
#16779=DIRECTION('center_axis',(1.43620113371566E-16,6.91638013500059E-17,
-1.));
#16780=DIRECTION('ref_axis',(0.623489801858732,0.781831482468031,1.43620113371566E-16));
#16781=DIRECTION('center_axis',(-1.43620113371566E-16,-6.91638013500059E-17,
1.));
#16782=DIRECTION('ref_axis',(0.623489801858732,0.781831482468031,1.43620113371566E-16));
#16783=DIRECTION('center_axis',(1.43620113371566E-16,6.91638013500059E-17,
-1.));
#16784=DIRECTION('ref_axis',(-0.623489801858732,-0.781831482468031,-1.43620113371566E-16));
#16785=DIRECTION('center_axis',(1.43620113371566E-16,6.91638013500059E-17,
-1.));
#16786=DIRECTION('ref_axis',(-0.623489801858732,-0.781831482468031,-1.43620113371566E-16));
#16787=DIRECTION('center_axis',(0.,0.,1.));
#16788=DIRECTION('ref_axis',(1.,0.,0.));
#16789=DIRECTION('center_axis',(0.,0.,-1.));
#16790=DIRECTION('ref_axis',(1.,0.,0.));
#16791=DIRECTION('center_axis',(0.,0.,1.));
#16792=DIRECTION('ref_axis',(1.,0.,0.));
#16793=DIRECTION('center_axis',(0.,0.,1.));
#16794=DIRECTION('ref_axis',(1.,0.,0.));
#16795=DIRECTION('center_axis',(0.,0.,-1.));
#16796=DIRECTION('ref_axis',(1.,0.,0.));
#16797=DIRECTION('center_axis',(0.,0.,1.));
#16798=DIRECTION('ref_axis',(1.,0.,0.));
#16799=DIRECTION('center_axis',(0.,0.,-1.));
#16800=DIRECTION('ref_axis',(-1.,0.,0.));
#16801=DIRECTION('center_axis',(0.,0.,-1.));
#16802=DIRECTION('ref_axis',(-1.,0.,0.));
#38024=CARTESIAN_POINT('',(0.,0.,0.));
#38025=CARTESIAN_POINT('Origin',(0.,1.73472347597681E-15,-6.67403582113016E-15));
#38026=CARTESIAN_POINT('',(1.52656933693714E-15,12.4653846153846,3.0875));
#38027=CARTESIAN_POINT('Origin',(0.,6.26866080313552E-16,3.0875));
#38028=CARTESIAN_POINT('',(-1.52656933693714E-15,12.4653846153846,-3.0875));
#38029=CARTESIAN_POINT('Origin',(-1.74512168878498E-15,14.25,-4.05635328795269E-15));
#38030=CARTESIAN_POINT('Origin',(0.,1.76119517802379E-15,-3.0875));
#38031=CARTESIAN_POINT('Origin',(0.,1.56496838953657E-16,5.64807088834312));
#38032=CARTESIAN_POINT('',(9.67029207191279E-16,7.64278544417155,5.99278544417156));
#38033=CARTESIAN_POINT('',(-9.35971273077467E-16,-7.64278544417155,5.99278544417156));
#38034=CARTESIAN_POINT('Origin',(0.,9.31738023414375E-17,5.99278544417156));
#38035=CARTESIAN_POINT('Origin',(0.,9.31738023414375E-17,5.99278544417156));
#38036=CARTESIAN_POINT('',(-9.18485099360515E-16,-7.5,5.64807088834312));
#38037=CARTESIAN_POINT('Origin',(-9.78186630818948E-16,-7.9875,5.64807088834312));
#38038=CARTESIAN_POINT('',(9.18485099360515E-16,7.5,5.64807088834312));
#38039=CARTESIAN_POINT('Origin',(0.,1.56496838953657E-16,5.64807088834312));
#38040=CARTESIAN_POINT('Origin',(0.,1.56496838953657E-16,5.64807088834312));
#38041=CARTESIAN_POINT('Origin',(0.,2.23156441938368E-15,-5.64807088834312));
#38042=CARTESIAN_POINT('',(9.18485099360515E-16,7.5,-5.64807088834312));
#38043=CARTESIAN_POINT('',(-9.18485099360515E-16,-7.5,-5.64807088834312));
#38044=CARTESIAN_POINT('Origin',(0.,2.23156441938368E-15,-5.64807088834312));
#38045=CARTESIAN_POINT('Origin',(0.,2.23156441938368E-15,-5.64807088834312));
#38046=CARTESIAN_POINT('',(-9.35971273077467E-16,-7.64278544417155,-5.99278544417156));
#38047=CARTESIAN_POINT('Origin',(-9.78186630818948E-16,-7.9875,-5.64807088834312));
#38048=CARTESIAN_POINT('Origin',(0.,2.2948874559959E-15,-5.99278544417156));
#38049=CARTESIAN_POINT('Origin',(0.,-9.99635681210842E-31,6.5));
#38050=CARTESIAN_POINT('',(-9.98087141305092E-16,8.14999999999999,6.50000000000001));
#38051=CARTESIAN_POINT('',(-9.98087141305092E-16,8.14999999999999,6.5));
#38052=CARTESIAN_POINT('Origin',(0.,-9.99635681210842E-31,6.5));
#38053=CARTESIAN_POINT('Origin',(0.,0.,6.5));
#38054=CARTESIAN_POINT('',(-9.18485099360515E-16,7.5,6.5));
#38055=CARTESIAN_POINT('Origin',(0.,2.26865819542047E-15,-5.85));
#38056=CARTESIAN_POINT('',(-9.98087141305091E-16,-8.14999999999998,-6.50000000000001));
#38057=CARTESIAN_POINT('',(-9.18485099360515E-16,-7.5,-5.85));
#38058=CARTESIAN_POINT('Origin',(0.,2.38806125833734E-15,-6.50000000000001));
#38059=CARTESIAN_POINT('Origin',(0.,0.,6.5));
#38060=CARTESIAN_POINT('',(-1.52656933693714E-15,12.4653846153846,-6.50000000000001));
#38061=CARTESIAN_POINT('',(-1.52656933693714E-15,12.4653846153846,6.5));
#38062=CARTESIAN_POINT('Origin',(0.,2.38806125833734E-15,-6.50000000000001));
#38063=CARTESIAN_POINT('Origin',(0.,0.,6.5));
#38064=CARTESIAN_POINT('',(-1.52656933693714E-15,12.4653846153846,6.50000000000001));
#38065=CARTESIAN_POINT('Origin',(0.,-1.17267830746035E-30,6.50000000000001));
#38066=CARTESIAN_POINT('',(-1.52656933693714E-15,12.4653846153846,6.5));
#38067=CARTESIAN_POINT('Origin',(0.,8.14999999999999,6.50000000000001));
#38068=CARTESIAN_POINT('Origin',(0.,8.14999999999999,-6.50000000000001));
#38069=CARTESIAN_POINT('Origin',(0.,14.25,-4.07195060716495E-15));
#38070=CARTESIAN_POINT('',(-3.56616156686793,14.25,-4.07195060716495E-15));
#38071=CARTESIAN_POINT('',(3.56616156686793,14.25,-4.07195060716495E-15));
#38072=CARTESIAN_POINT('Origin',(0.,14.25,-4.07195060716495E-15));
#38073=CARTESIAN_POINT('Origin',(11.1410986251694,8.88472967648693,-5.05753477640253E-15));
#38074=CARTESIAN_POINT('',(8.91763325644669,11.6728670610318,-4.54536224786764E-15));
#38075=CARTESIAN_POINT('',(13.3645639938921,6.09659229194206,-5.56970730493742E-15));
#38076=CARTESIAN_POINT('Origin',(11.1410986251694,8.88472967648693,-5.05753477640253E-15));
#38077=CARTESIAN_POINT('Origin',(13.892722748591,-3.17092330887753,-7.27212230242621E-15));
#38078=CARTESIAN_POINT('',(14.6862683510896,0.305827142012077,-6.6334536057588E-15));
#38079=CARTESIAN_POINT('',(13.0991771460924,-6.64767375976714,-7.91079099909362E-15));
#38080=CARTESIAN_POINT('Origin',(13.892722748591,-3.17092330887753,-7.27212230242621E-15));
#38081=CARTESIAN_POINT('Origin',(6.18284328242512,-12.8388063676095,-9.04808360878726E-15));
#38082=CARTESIAN_POINT('',(9.39584383208325,-11.2915068526795,-8.76384929904507E-15));
#38083=CARTESIAN_POINT('',(2.96984273276699,-14.3861058825395,-9.33231791852945E-15));
#38084=CARTESIAN_POINT('Origin',(6.18284328242512,-12.8388063676095,-9.04808360878726E-15));
#38085=CARTESIAN_POINT('Origin',(-6.1828432824253,-12.8388063676094,-9.04808360878725E-15));
#38086=CARTESIAN_POINT('',(-2.9698427327672,-14.3861058825394,-9.33231791852944E-15));
#38087=CARTESIAN_POINT('',(-9.39584383208341,-11.2915068526794,-8.76384929904506E-15));
#38088=CARTESIAN_POINT('Origin',(-6.1828432824253,-12.8388063676094,-9.04808360878725E-15));
#38089=CARTESIAN_POINT('Origin',(-13.892722748591,-3.17092330887735,-7.27212230242617E-15));
#38090=CARTESIAN_POINT('',(-13.0991771460925,-6.64767375976697,-7.91079099909359E-15));
#38091=CARTESIAN_POINT('',(-14.6862683510895,0.30582714201227,-6.63345360575876E-15));
#38092=CARTESIAN_POINT('Origin',(-13.892722748591,-3.17092330887735,-7.27212230242617E-15));
#38093=CARTESIAN_POINT('Origin',(-11.1410986251693,8.88472967648709,-5.0575347764025E-15));
#38094=CARTESIAN_POINT('',(-13.3645639938921,6.09659229194225,-5.56970730493739E-15));
#38095=CARTESIAN_POINT('',(-8.91763325644655,11.6728670610319,-4.54536224786761E-15));
#38096=CARTESIAN_POINT('Origin',(-11.1410986251693,8.88472967648709,-5.0575347764025E-15));
#38097=CARTESIAN_POINT('Origin',(0.,1.07462756625201E-17,6.44149999999999));
#38098=CARTESIAN_POINT('',(-1.99949495950787E-15,-16.3271153846154,6.49999999999999));
#38099=CARTESIAN_POINT('Origin',(0.,2.01169401222323E-30,6.49999999999999));
#38100=CARTESIAN_POINT('',(-1.99233077573286E-15,-16.2686153846154,6.44149999999999));
#38101=CARTESIAN_POINT('Origin',(-1.99949495950788E-15,-16.3271153846154,
6.44149999999999));
#38102=CARTESIAN_POINT('',(1.99233077573286E-15,16.2686153846154,6.44149999999999));
#38103=CARTESIAN_POINT('Origin',(0.,1.07462756625199E-17,6.44149999999999));
#38104=CARTESIAN_POINT('Origin',(0.,1.07462756625199E-17,6.44149999999999));
#38105=CARTESIAN_POINT('Origin',(0.,1.30149338579385E-16,5.7915));
#38106=CARTESIAN_POINT('',(-1.96367404063281E-15,16.0346153846154,5.7915));
#38107=CARTESIAN_POINT('Origin',(0.,1.30149338579385E-16,5.7915));
#38108=CARTESIAN_POINT('',(-1.97083822440782E-15,16.0931153846154,5.85));
#38109=CARTESIAN_POINT('Origin',(-1.97083822440783E-15,16.0931153846154,
5.7915));
#38110=CARTESIAN_POINT('Origin',(0.,1.19403062916867E-16,5.85));
#38111=CARTESIAN_POINT('Origin',(0.,2.37731498267482E-15,-6.44150000000001));
#38112=CARTESIAN_POINT('',(-1.99949495950787E-15,16.3271153846154,-6.5));
#38113=CARTESIAN_POINT('Origin',(0.,2.38806125833734E-15,-6.50000000000001));
#38114=CARTESIAN_POINT('',(-1.99233077573286E-15,16.2686153846154,-6.4415));
#38115=CARTESIAN_POINT('Origin',(-1.99949495950788E-15,16.3271153846154,
-6.44150000000001));
#38116=CARTESIAN_POINT('Origin',(0.,2.37731498267482E-15,-6.44150000000001));
#38117=CARTESIAN_POINT('Origin',(0.,2.25791191975795E-15,-5.7915));
#38118=CARTESIAN_POINT('',(1.96367404063281E-15,16.0346153846154,-5.7915));
#38119=CARTESIAN_POINT('',(-1.96367404063282E-15,-16.0346153846154,-5.7915));
#38120=CARTESIAN_POINT('Origin',(0.,2.25791191975795E-15,-5.7915));
#38121=CARTESIAN_POINT('Origin',(0.,2.25791191975795E-15,-5.7915));
#38122=CARTESIAN_POINT('',(-1.97083822440782E-15,-16.0931153846154,-5.85000000000001));
#38123=CARTESIAN_POINT('Origin',(-1.97083822440783E-15,-16.0931153846154,
-5.7915));
#38124=CARTESIAN_POINT('Origin',(0.,2.26865819542047E-15,-5.85));
#38125=CARTESIAN_POINT('Origin',(0.,0.,6.5));
#38126=CARTESIAN_POINT('',(-2.16636878649169E-15,17.6897435897436,5.85));
#38127=CARTESIAN_POINT('Origin',(0.,1.19403062916867E-16,5.85));
#38128=CARTESIAN_POINT('',(-2.16636878649169E-15,17.6897435897436,6.084));
#38129=CARTESIAN_POINT('',(-2.16636878649169E-15,17.6897435897436,6.5));
#38130=CARTESIAN_POINT('Origin',(0.,7.6417960266795E-17,6.084));
#38131=CARTESIAN_POINT('Origin',(0.,0.,6.5));
#38132=CARTESIAN_POINT('',(-1.99233077573286E-15,16.2686153846154,6.084));
#38133=CARTESIAN_POINT('Origin',(0.,7.6417960266795E-17,6.084));
#38134=CARTESIAN_POINT('',(-1.99233077573286E-15,16.2686153846154,6.5));
#38135=CARTESIAN_POINT('Origin',(0.,0.,6.5));
#38136=CARTESIAN_POINT('',(-1.96367404063281E-15,16.0346153846154,-3.0875));
#38137=CARTESIAN_POINT('',(-1.96367404063282E-15,16.0346153846154,6.5));
#38138=CARTESIAN_POINT('Origin',(0.,1.76119517802379E-15,-3.08750000000001));
#38139=CARTESIAN_POINT('Origin',(0.,1.73472347597681E-15,-6.67403582113016E-15));
#38140=CARTESIAN_POINT('',(-1.96367404063281E-15,16.0346153846154,3.0875));
#38141=CARTESIAN_POINT('Origin',(-1.74512168878498E-15,14.25,-4.05635328795269E-15));
#38142=CARTESIAN_POINT('Origin',(0.,6.26866080313552E-16,3.08749999999999));
#38143=CARTESIAN_POINT('Origin',(0.,0.,6.5));
#38144=CARTESIAN_POINT('',(-1.96367404063282E-15,16.0346153846154,6.5));
#38145=CARTESIAN_POINT('Origin',(0.,0.,6.5));
#38146=CARTESIAN_POINT('',(-1.99233077573286E-15,16.2686153846154,-6.084));
#38147=CARTESIAN_POINT('',(-1.99233077573286E-15,16.2686153846154,6.5));
#38148=CARTESIAN_POINT('Origin',(0.,2.31164329807054E-15,-6.084));
#38149=CARTESIAN_POINT('Origin',(0.,0.,6.5));
#38150=CARTESIAN_POINT('',(-2.16636878649169E-15,17.6897435897436,-6.084));
#38151=CARTESIAN_POINT('Origin',(0.,2.31164329807054E-15,-6.084));
#38152=CARTESIAN_POINT('',(-2.16636878649169E-15,17.6897435897436,-5.85));
#38153=CARTESIAN_POINT('',(-2.16636878649169E-15,17.6897435897436,6.5));
#38154=CARTESIAN_POINT('Origin',(0.,2.26865819542047E-15,-5.85));
#38155=CARTESIAN_POINT('Origin',(0.,2.38806125833734E-15,-6.50000000000001));
#38156=CARTESIAN_POINT('',(-2.57175827820944E-15,21.,-5.85));
#38157=CARTESIAN_POINT('Origin',(0.,2.26865819542047E-15,-5.85000000000001));
#38158=CARTESIAN_POINT('',(-2.49215623626487E-15,20.35,-6.5));
#38159=CARTESIAN_POINT('',(-2.49215623626486E-15,20.35,-6.50000000000001));
#38160=CARTESIAN_POINT('Origin',(0.,2.38806125833734E-15,-6.50000000000001));
#38161=CARTESIAN_POINT('Origin',(0.,1.19403062916869E-16,5.84999999999999));
#38162=CARTESIAN_POINT('',(2.57175827820944E-15,21.,5.84999999999999));
#38163=CARTESIAN_POINT('',(-2.57175827820944E-15,-21.,5.84999999999999));
#38164=CARTESIAN_POINT('Origin',(0.,1.19403062916869E-16,5.84999999999999));
#38165=CARTESIAN_POINT('',(-2.49215623626487E-15,-20.35,6.49999999999999));
#38166=CARTESIAN_POINT('',(-2.57175827820944E-15,-21.,5.84999999999999));
#38167=CARTESIAN_POINT('Origin',(0.,1.96135664184276E-30,6.49999999999999));
#38168=CARTESIAN_POINT('Origin',(0.,1.19403062916869E-16,5.84999999999999));
#38169=CARTESIAN_POINT('Origin',(0.,0.,6.5));
#38170=CARTESIAN_POINT('',(-2.57175827820944E-15,21.,6.5));
#38171=CARTESIAN_POINT('Origin',(0.,20.35,6.49999999999999));
#38172=CARTESIAN_POINT('Origin',(0.,20.35,-6.5));
#38173=CARTESIAN_POINT('Origin',(0.,16.0346153846154,-5.85));
#38174=CARTESIAN_POINT('Origin',(0.,16.2686153846154,-6.084));
#38175=CARTESIAN_POINT('Origin',(0.,16.2686153846154,6.084));
#38176=CARTESIAN_POINT('Origin',(0.,16.0346153846154,5.85));
#38177=CARTESIAN_POINT('Origin',(-11.1410986251694,8.88472967648693,-9.85584169237584E-16));
#38178=CARTESIAN_POINT('',(-11.838732871064,9.44107442276088,-3.96060240207311));
#38179=CARTESIAN_POINT('Origin',(-11.838732871064,9.44107442276088,-1.04729956121144E-15));
#38180=CARTESIAN_POINT('',(-10.4434643792749,8.32838493021299,-3.96060240207311));
#38181=CARTESIAN_POINT('Origin',(-11.1410986251694,8.88472967648693,-2.5198520116158));
#38182=CARTESIAN_POINT('Origin',(-10.4434643792749,8.32838493021299,-9.23868777263733E-16));
#38183=CARTESIAN_POINT('',(-13.176267261227,5.42664547033602,1.08333333333333));
#38184=CARTESIAN_POINT('',(-13.9269936544441,5.94376395877182,1.08333333333333));
#38185=CARTESIAN_POINT('Ctrl Pts',(-13.176267261227,5.42664547033603,1.08333333333333));
#38186=CARTESIAN_POINT('Ctrl Pts',(-13.3544742809805,5.48608062863209,1.08333333333333));
#38187=CARTESIAN_POINT('Ctrl Pts',(-13.5395781511317,5.58798093945111,1.08333333333333));
#38188=CARTESIAN_POINT('Ctrl Pts',(-13.7657237213497,5.76832601371359,1.08333333333333));
#38189=CARTESIAN_POINT('Ctrl Pts',(-13.851789663848,5.85187873682469,1.08333333333333));
#38190=CARTESIAN_POINT('Ctrl Pts',(-13.9269936544446,5.9437639587714,1.08333333333333));
#38191=CARTESIAN_POINT('',(-13.176267261227,5.42664547033602,-1.08333333333333));
#38192=CARTESIAN_POINT('Ctrl Pts',(-13.176267261227,5.426645470336,1.08333333333333));
#38193=CARTESIAN_POINT('Ctrl Pts',(-13.1893705593041,5.39482976422217,0.949270311030458));
#38194=CARTESIAN_POINT('Ctrl Pts',(-13.1999097963793,5.36892368585873,0.813521288367943));
#38195=CARTESIAN_POINT('Ctrl Pts',(-13.2079621630869,5.34904061477063,0.676607052100963));
#38196=CARTESIAN_POINT('Ctrl Pts',(-13.2148460430323,5.33204279546006,0.559560573777783));
#38197=CARTESIAN_POINT('Ctrl Pts',(-13.2199117356377,5.31944645364942,0.441662516279014));
#38198=CARTESIAN_POINT('Ctrl Pts',(-13.2231796369648,5.31131059989529,0.323238258334693));
#38199=CARTESIAN_POINT('Ctrl Pts',(-13.2269557156994,5.30190957419894,0.186398348762648));
#38200=CARTESIAN_POINT('Ctrl Pts',(-13.2283213471704,5.29849241313602,0.0492519096262365));
#38201=CARTESIAN_POINT('Ctrl Pts',(-13.2273014856384,5.30103720115478,-0.0876758270660023));
#38202=CARTESIAN_POINT('Ctrl Pts',(-13.2262786675027,5.30358936657696,-0.225000520654269));
#38203=CARTESIAN_POINT('Ctrl Pts',(-13.2228564747501,5.31213809759637,-0.362105241912721));
#38204=CARTESIAN_POINT('Ctrl Pts',(-13.21701132539,5.32664168351063,-0.498460177595569));
#38205=CARTESIAN_POINT('Ctrl Pts',(-13.2111409592134,5.34120783998416,-0.635403368116636));
#38206=CARTESIAN_POINT('Ctrl Pts',(-13.2028266475275,5.36178038996277,-0.771590289741212));
#38207=CARTESIAN_POINT('Ctrl Pts',(-13.1919958930595,5.38829698119001,-0.90648424252654));
#38208=CARTESIAN_POINT('Ctrl Pts',(-13.1872415508606,5.39993688577963,-0.965698216399817));
#38209=CARTESIAN_POINT('Ctrl Pts',(-13.1820016856382,5.4127218947045,-1.02466304565395));
#38210=CARTESIAN_POINT('Ctrl Pts',(-13.176267261227,5.426645470336,-1.08333333333333));
#38211=CARTESIAN_POINT('',(-13.9269936544455,5.94376395877242,-1.08333333333333));
#38212=CARTESIAN_POINT('Ctrl Pts',(-13.176267261227,5.42664547033603,-1.08333333333333));
#38213=CARTESIAN_POINT('Ctrl Pts',(-13.3544742809805,5.48608062863209,-1.08333333333333));
#38214=CARTESIAN_POINT('Ctrl Pts',(-13.5395781511317,5.58798093945111,-1.08333333333333));
#38215=CARTESIAN_POINT('Ctrl Pts',(-13.76572372135,5.76832601371385,-1.08333333333333));
#38216=CARTESIAN_POINT('Ctrl Pts',(-13.8517896638487,5.85187873682532,-1.08333333333333));
#38217=CARTESIAN_POINT('Ctrl Pts',(-13.9269936544455,5.94376395877245,-1.08333333333333));
#38218=CARTESIAN_POINT('Ctrl Pts',(-13.9269936544444,5.94376395877114,-1.08333333333355));
#38219=CARTESIAN_POINT('Ctrl Pts',(-13.9416885168396,5.90933203032471,-0.95688863210348));
#38220=CARTESIAN_POINT('Ctrl Pts',(-13.9536527109306,5.88095561854246,-0.828820583351296));
#38221=CARTESIAN_POINT('Ctrl Pts',(-13.9629765258054,5.85873440158612,-0.699646919261824));
#38222=CARTESIAN_POINT('Ctrl Pts',(-13.9722513158078,5.83663002439321,-0.571152453813156));
#38223=CARTESIAN_POINT('Ctrl Pts',(-13.9789135007646,5.82061622745832,-0.441563969171476));
#38224=CARTESIAN_POINT('Ctrl Pts',(-13.9830050237945,5.81077040959789,-0.311391073637591));
#38225=CARTESIAN_POINT('Ctrl Pts',(-13.9870637119681,5.80100360534983,-0.182262827807202));
#38226=CARTESIAN_POINT('Ctrl Pts',(-13.9885928700523,5.79730615639837,-0.0525595133518154));
#38227=CARTESIAN_POINT('Ctrl Pts',(-13.9875862925321,5.79973378332902,0.0772214321948836));
#38228=CARTESIAN_POINT('Ctrl Pts',(-13.9868997670034,5.80138952054624,0.16573715053464));
#38229=CARTESIAN_POINT('Ctrl Pts',(-13.9850326975558,5.80589410253377,0.25428898113034));
#38230=CARTESIAN_POINT('Ctrl Pts',(-13.9819702480149,5.81325986277477,0.342719102199523));
#38231=CARTESIAN_POINT('Ctrl Pts',(-13.9773533484511,5.82436436418404,0.476034927301742));
#38232=CARTESIAN_POINT('Ctrl Pts',(-13.9700489046451,5.84190742581559,0.608312350205735));
#38233=CARTESIAN_POINT('Ctrl Pts',(-13.9600480872369,5.86570879353503,0.739057191237609));
#38234=CARTESIAN_POINT('Ctrl Pts',(-13.9511688384278,5.8868408927778,0.855139299994326));
#38235=CARTESIAN_POINT('Ctrl Pts',(-13.9401632237806,5.9129059856334,0.970013302477931));
#38236=CARTESIAN_POINT('Ctrl Pts',(-13.9269936544444,5.94376395877114,1.08333333333355));
#38237=CARTESIAN_POINT('',(-8.89378902201695,12.2552029391753,1.08333333333333));
#38238=CARTESIAN_POINT('',(-8.22258343557141,11.6383685130291,1.08333333333333));
#38239=CARTESIAN_POINT('Ctrl Pts',(-8.89378902201693,12.2552029391753,1.08333333333333));
#38240=CARTESIAN_POINT('Ctrl Pts',(-8.78747309219938,12.2023308550396,1.08333333333333));
#38241=CARTESIAN_POINT('Ctrl Pts',(-8.68686373639314,12.1370149953911,1.08333333333333));
#38242=CARTESIAN_POINT('Ctrl Pts',(-8.46071816617524,11.9566699211287,1.08333333333333));
#38243=CARTESIAN_POINT('Ctrl Pts',(-8.32018322283281,11.7988819437994,1.08333333333333));
#38244=CARTESIAN_POINT('Ctrl Pts',(-8.22258343557192,11.6383685130288,1.08333333333333));
#38245=CARTESIAN_POINT('',(-8.89378902201695,12.2552029391753,-1.08333333333333));
#38246=CARTESIAN_POINT('Ctrl Pts',(-8.89378902201696,12.2552029391753,1.08333333333333));
#38247=CARTESIAN_POINT('Ctrl Pts',(-8.86325700199161,12.2773604951023,0.955915065626613));
#38248=CARTESIAN_POINT('Ctrl Pts',(-8.83806624000395,12.2954729083691,0.8267015714506));
#38249=CARTESIAN_POINT('Ctrl Pts',(-8.81837639229442,12.3095783864577,0.696211209492237));
#38250=CARTESIAN_POINT('Ctrl Pts',(-8.79899689851553,12.3234615321731,0.567777653525536));
#38251=CARTESIAN_POINT('Ctrl Pts',(-8.7849462329058,12.3334631509294,0.438107164856251));
#38252=CARTESIAN_POINT('Ctrl Pts',(-8.77634666705863,12.3395794672318,0.307693975181527));
#38253=CARTESIAN_POINT('Ctrl Pts',(-8.76960830208466,12.3443720314467,0.205506064179221));
#38254=CARTESIAN_POINT('Ctrl Pts',(-8.76621624622179,12.3467783236356,0.102862147741002));
#38255=CARTESIAN_POINT('Ctrl Pts',(-8.76621624622179,12.3467783236356,-2.44249065417534E-15));
#38256=CARTESIAN_POINT('Ctrl Pts',(-8.76621624622179,12.3467783236356,-0.130666807305558));
#38257=CARTESIAN_POINT('Ctrl Pts',(-8.77169236507929,12.3428956683044,-0.261069786498707));
#38258=CARTESIAN_POINT('Ctrl Pts',(-8.78256611126601,12.3351536167882,-0.390710450871087));
#38259=CARTESIAN_POINT('Ctrl Pts',(-8.79357042167237,12.3273186042172,-0.521907748246256));
#38260=CARTESIAN_POINT('Ctrl Pts',(-8.8101027782242,12.315530900308,-0.652324314224256));
#38261=CARTESIAN_POINT('Ctrl Pts',(-8.83205039902736,12.2997710546807,-0.781443489202971));
#38262=CARTESIAN_POINT('Ctrl Pts',(-8.84930597782606,12.2873804060307,-0.882959098491573));
#38263=CARTESIAN_POINT('Ctrl Pts',(-8.86990830867396,12.2725335396739,-0.983672743459536));
#38264=CARTESIAN_POINT('Ctrl Pts',(-8.89378902201696,12.2552029391753,-1.08333333333333));
#38265=CARTESIAN_POINT('',(-8.22258343557665,11.6383685130365,-1.08333333333333));
#38266=CARTESIAN_POINT('Ctrl Pts',(-8.89378902201693,12.2552029391753,-1.08333333333333));
#38267=CARTESIAN_POINT('Ctrl Pts',(-8.78747309219938,12.2023308550396,-1.08333333333333));
#38268=CARTESIAN_POINT('Ctrl Pts',(-8.68686373639314,12.1370149953911,-1.08333333333333));
#38269=CARTESIAN_POINT('Ctrl Pts',(-8.46071816617751,11.9566699211305,-1.08333333333333));
#38270=CARTESIAN_POINT('Ctrl Pts',(-8.32018322283717,11.7988819438045,-1.08333333333333));
#38271=CARTESIAN_POINT('Ctrl Pts',(-8.22258343557662,11.6383685130365,-1.08333333333333));
#38272=CARTESIAN_POINT('Ctrl Pts',(-8.22258343557191,11.6383685130287,-1.08333333333318));
#38273=CARTESIAN_POINT('Ctrl Pts',(-8.19455490688727,11.6581708517696,-0.949622058007629));
#38274=CARTESIAN_POINT('Ctrl Pts',(-8.17172113698899,11.6741565633286,-0.814376693553349));
#38275=CARTESIAN_POINT('Ctrl Pts',(-8.15417398891324,11.6864000683928,-0.678132403728345));
#38276=CARTESIAN_POINT('Ctrl Pts',(-8.13671023659264,11.698585384152,-0.542535637671064));
#38277=CARTESIAN_POINT('Ctrl Pts',(-8.12448291951145,11.7070640382822,-0.405949418799179));
#38278=CARTESIAN_POINT('Ctrl Pts',(-8.11755242812626,11.7118675955896,-0.268901316712111));
#38279=CARTESIAN_POINT('Ctrl Pts',(-8.11302715126356,11.7150040870061,-0.179415511018989));
#38280=CARTESIAN_POINT('Ctrl Pts',(-8.11075954642953,11.7165728598427,-0.0897327832367744));
#38281=CARTESIAN_POINT('Ctrl Pts',(-8.11075954642953,11.7165728598427,-9.99200722162641E-15));
#38282=CARTESIAN_POINT('Ctrl Pts',(-8.11075954642954,11.7165728598427,0.137573936980354));
#38283=CARTESIAN_POINT('Ctrl Pts',(-8.11609005089583,11.7128881555246,0.274951212619692));
#38284=CARTESIAN_POINT('Ctrl Pts',(-8.12669452775723,11.7055258768037,0.4116124062147));
#38285=CARTESIAN_POINT('Ctrl Pts',(-8.13738105388554,11.6981066344457,0.549330978772881));
#38286=CARTESIAN_POINT('Ctrl Pts',(-8.15342350530942,11.6869526399855,0.686322345437031));
#38287=CARTESIAN_POINT('Ctrl Pts',(-8.17473347641523,11.6720277839618,0.822054935347404));
#38288=CARTESIAN_POINT('Ctrl Pts',(-8.18849695174643,11.662388264195,0.909720570537357));
#38289=CARTESIAN_POINT('Ctrl Pts',(-8.20445714658991,11.6511748546878,0.996861109122827));
#38290=CARTESIAN_POINT('Ctrl Pts',(-8.22258343557191,11.6383685130287,1.08333333333318));
#38291=CARTESIAN_POINT('Origin',(-11.1410986251694,8.88472967648693,-9.85584169237584E-16));
#38292=CARTESIAN_POINT('',(-13.6377879061429,6.58029051604744,-1.08333333333333));
#38293=CARTESIAN_POINT('',(-13.2594869773434,6.22835470309403,-1.08333333333333));
#38294=CARTESIAN_POINT('Origin',(-11.1410986251694,8.88472967648693,-1.08333333333333));
#38295=CARTESIAN_POINT('',(-9.02271027299537,11.5411046498798,-1.08333333333333));
#38296=CARTESIAN_POINT('Origin',(-11.1410986251694,8.88472967648693,-9.85584169237584E-16));
#38297=CARTESIAN_POINT('',(-9.45000219633307,11.8316076987796,-1.08333333333333));
#38298=CARTESIAN_POINT('Origin',(-11.1410986251694,8.88472967648693,-1.08333333333333));
#38299=CARTESIAN_POINT('',(-9.45000219633307,11.8316076987796,1.08333333333333));
#38300=CARTESIAN_POINT('Ctrl Pts',(-9.45000219633306,11.8316076987796,-1.08333333333334));
#38301=CARTESIAN_POINT('Ctrl Pts',(-9.35474240837113,11.9076924734257,-0.727666221822799));
#38302=CARTESIAN_POINT('Ctrl Pts',(-9.30796390402501,11.9436715548398,-0.352782973842778));
#38303=CARTESIAN_POINT('Ctrl Pts',(-9.30796390402501,11.9436715548398,-5.10741104345864E-16));
#38304=CARTESIAN_POINT('Ctrl Pts',(-9.30796390402501,11.9436715548398,0.352782973842777));
#38305=CARTESIAN_POINT('Ctrl Pts',(-9.35474240837113,11.9076924734257,0.727666221822798));
#38306=CARTESIAN_POINT('Ctrl Pts',(-9.45000219633306,11.8316076987796,1.08333333333334));
#38307=CARTESIAN_POINT('',(-8.72113759169224,11.2696166353063,1.08333333333333));
#38308=CARTESIAN_POINT('Origin',(-11.1410986251694,8.88472967648693,1.08333333333333));
#38309=CARTESIAN_POINT('',(-8.72113759169224,11.2696166353063,-1.08333333333333));
#38310=CARTESIAN_POINT('Ctrl Pts',(-8.72113759169222,11.2696166353063,1.08333333333334));
#38311=CARTESIAN_POINT('Ctrl Pts',(-8.63036626326988,11.3398611937656,0.725928647976584));
#38312=CARTESIAN_POINT('Ctrl Pts',(-8.58623309669495,11.3727349924818,0.352039859176991));
#38313=CARTESIAN_POINT('Ctrl Pts',(-8.58623309669495,11.3727349924818,-4.46574186955748E-16));
#38314=CARTESIAN_POINT('Ctrl Pts',(-8.58623309669495,11.3727349924818,-0.352039859176992));
#38315=CARTESIAN_POINT('Ctrl Pts',(-8.63036626326988,11.3398611937656,-0.725928647976585));
#38316=CARTESIAN_POINT('Ctrl Pts',(-8.72113759169222,11.2696166353063,-1.08333333333334));
#38317=CARTESIAN_POINT('Origin',(-11.1410986251694,8.88472967648693,-1.08333333333333));
#38318=CARTESIAN_POINT('',(-12.9276994994136,5.99475484510091,-1.08333333333333));
#38319=CARTESIAN_POINT('Origin',(-11.1410986251694,8.88472967648693,-1.08333333333333));
#38320=CARTESIAN_POINT('',(-12.9276994994136,5.99475484510091,1.08333333333333));
#38321=CARTESIAN_POINT('Ctrl Pts',(-12.9276994994136,5.99475484510092,-1.08333333333333));
#38322=CARTESIAN_POINT('Ctrl Pts',(-12.9759843593574,5.89062845864246,-0.725928647976576));
#38323=CARTESIAN_POINT('Ctrl Pts',(-12.9982133898606,5.84028669430256,-0.352039859176989));
#38324=CARTESIAN_POINT('Ctrl Pts',(-12.9982133898606,5.84028669430256,0.352039859176986));
#38325=CARTESIAN_POINT('Ctrl Pts',(-12.9759843593574,5.89062845864246,0.725928647976574));
#38326=CARTESIAN_POINT('Ctrl Pts',(-12.9276994994136,5.99475484510092,1.08333333333332));
#38327=CARTESIAN_POINT('',(-13.6377879061429,6.58029051604744,1.08333333333333));
#38328=CARTESIAN_POINT('Origin',(-11.1410986251694,8.88472967648693,1.08333333333333));
#38329=CARTESIAN_POINT('Ctrl Pts',(-13.6377879061429,6.58029051604746,1.08333333333332));
#38330=CARTESIAN_POINT('Ctrl Pts',(-13.6907677796516,6.47048863474076,0.727666221822783));
#38331=CARTESIAN_POINT('Ctrl Pts',(-13.7154355939007,6.41687686636447,0.352782973842769));
#38332=CARTESIAN_POINT('Ctrl Pts',(-13.7154355939007,6.41687686636447,-0.352782973842771));
#38333=CARTESIAN_POINT('Ctrl Pts',(-13.6907677796516,6.47048863474076,-0.727666221822784));
#38334=CARTESIAN_POINT('Ctrl Pts',(-13.6377879061429,6.58029051604746,-1.08333333333332));
#38335=CARTESIAN_POINT('',(-10.4434643792749,8.32838493021299,3.45272288248773));
#38336=CARTESIAN_POINT('Origin',(-10.4434643792749,8.32838493021299,-9.23868777263733E-16));
#38337=CARTESIAN_POINT('',(-11.838732871064,9.44107442276088,3.45272288248773));
#38338=CARTESIAN_POINT('Origin',(-11.838732871064,9.44107442276088,-1.04729956121144E-15));
#38339=CARTESIAN_POINT('Origin',(-13.892722748591,-3.17092330887753,-3.20017169526126E-15));
#38340=CARTESIAN_POINT('',(-14.7626584240763,-3.36948044994625,-3.96060240207311));
#38341=CARTESIAN_POINT('Origin',(-14.7626584240763,-3.36948044994625,-3.40056031423578E-15));
#38342=CARTESIAN_POINT('',(-13.0227870731057,-2.97236616780882,-3.96060240207311));
#38343=CARTESIAN_POINT('Origin',(-13.892722748591,-3.17092330887753,-2.5198520116158));
#38344=CARTESIAN_POINT('Origin',(-13.0227870731057,-2.97236616780882,-2.99978307628674E-15));
#38345=CARTESIAN_POINT('',(-12.4579905368413,-6.91816245718267,1.08333333333333));
#38346=CARTESIAN_POINT('',(-13.3303603014234,-7.18268588222789,1.08333333333333));
#38347=CARTESIAN_POINT('Ctrl Pts',(-12.4579905368413,-6.91816245718265,
1.08333333333333));
#38348=CARTESIAN_POINT('Ctrl Pts',(-12.6155690741986,-7.02043310055334,
1.08333333333333));
#38349=CARTESIAN_POINT('Ctrl Pts',(-12.8106483205941,-7.10161932916232,
1.08333333333333));
#38350=CARTESIAN_POINT('Ctrl Pts',(-13.0926472341269,-7.16598374096129,
1.08333333333333));
#38351=CARTESIAN_POINT('Ctrl Pts',(-13.211632620936,-7.18117853359748,1.08333333333333));
#38352=CARTESIAN_POINT('Ctrl Pts',(-13.3303603014234,-7.18268588222786,
1.08333333333333));
#38353=CARTESIAN_POINT('',(-12.4579905368413,-6.91816245718267,-1.08333333333334));
#38354=CARTESIAN_POINT('Ctrl Pts',(-12.4579905368413,-6.91816245718269,
1.08333333333333));
#38355=CARTESIAN_POINT('Ctrl Pts',(-12.4412857888864,-6.94824379644449,
0.949270311030495));
#38356=CARTESIAN_POINT('Ctrl Pts',(-12.4276027080703,-6.97263587945683,
0.813521288368019));
#38357=CARTESIAN_POINT('Ctrl Pts',(-12.4170780656485,-6.99132836531023,
0.676607052101084));
#38358=CARTESIAN_POINT('Ctrl Pts',(-12.4080806643214,-7.0073083663671,0.559560573777871));
#38359=CARTESIAN_POINT('Ctrl Pts',(-12.4013908554087,-7.01912257498617,
0.441662516279072));
#38360=CARTESIAN_POINT('Ctrl Pts',(-12.3970674919579,-7.02675014497037,
0.323238258334728));
#38361=CARTESIAN_POINT('Ctrl Pts',(-12.392071820683,-7.03556384585404,0.186398348762656));
#38362=CARTESIAN_POINT('Ctrl Pts',(-12.3902516338786,-7.03876210460556,
0.0492519096262199));
#38363=CARTESIAN_POINT('Ctrl Pts',(-12.3916053560034,-7.03637809537454,
-0.0876758270660418));
#38364=CARTESIAN_POINT('Ctrl Pts',(-12.3929630026022,-7.03398717484178,
-0.22500052065431));
#38365=CARTESIAN_POINT('Ctrl Pts',(-12.3975129673671,-7.02598155019929,
-0.36210524191276));
#38366=CARTESIAN_POINT('Ctrl Pts',(-12.4052079364271,-7.0123687905019,-0.498460177595606));
#38367=CARTESIAN_POINT('Ctrl Pts',(-12.4129361026924,-6.99869730339788,
-0.635403368116707));
#38368=CARTESIAN_POINT('Ctrl Pts',(-12.4238364813948,-6.97937013765694,
-0.771590289741313));
#38369=CARTESIAN_POINT('Ctrl Pts',(-12.4378151222667,-6.9543694886247,-0.906484242526672));
#38370=CARTESIAN_POINT('Ctrl Pts',(-12.4439512822522,-6.94339503240897,
-0.965698216399908));
#38371=CARTESIAN_POINT('Ctrl Pts',(-12.450680002204,-6.93132701813286,-1.024663045654));
#38372=CARTESIAN_POINT('Ctrl Pts',(-12.4579905368413,-6.91816245718269,
-1.08333333333334));
#38373=CARTESIAN_POINT('',(-13.3303603014234,-7.18268588222787,-1.08333333333334));
#38374=CARTESIAN_POINT('Ctrl Pts',(-12.4579905368413,-6.91816245718265,
-1.08333333333333));
#38375=CARTESIAN_POINT('Ctrl Pts',(-12.6150882655077,-7.02012104908378,
-1.08333333333333));
#38376=CARTESIAN_POINT('Ctrl Pts',(-12.8106174809568,-7.10161229021636,
-1.08333333333333));
#38377=CARTESIAN_POINT('Ctrl Pts',(-13.0925863122299,-7.16596983593587,
-1.08333333333333));
#38378=CARTESIAN_POINT('Ctrl Pts',(-13.2116839714656,-7.18117918553602,
-1.08333333333333));
#38379=CARTESIAN_POINT('Ctrl Pts',(-13.3303603014234,-7.18268588222786,
-1.08333333333333));
#38380=CARTESIAN_POINT('Ctrl Pts',(-13.3303603014234,-7.18268588222788,
-1.08333333333333));
#38381=CARTESIAN_POINT('Ctrl Pts',(-13.312602432605,-7.21564274452362,-0.9568886321034));
#38382=CARTESIAN_POINT('Ctrl Pts',(-13.2978764135175,-7.24268913148589,
-0.828820583351364));
#38383=CARTESIAN_POINT('Ctrl Pts',(-13.2863164700111,-7.26383348564883,
-0.699646919262042));
#38384=CARTESIAN_POINT('Ctrl Pts',(-13.2748173090022,-7.28486666222222,
-0.571152453813466));
#38385=CARTESIAN_POINT('Ctrl Pts',(-13.2664510227833,-7.30005980724142,
-0.441563969171881));
#38386=CARTESIAN_POINT('Ctrl Pts',(-13.2613042752926,-7.30939745578436,
-0.311391073638092));
#38387=CARTESIAN_POINT('Ctrl Pts',(-13.2561988309335,-7.3186601688214,-0.182262827807686));
#38388=CARTESIAN_POINT('Ctrl Pts',(-13.2542614634094,-7.32216103446744,
-0.0525595133522827));
#38389=CARTESIAN_POINT('Ctrl Pts',(-13.2555318677528,-7.31986045983868,
0.0772214321944347));
#38390=CARTESIAN_POINT('Ctrl Pts',(-13.2563983335701,-7.31829137729732,
0.165737150534351));
#38391=CARTESIAN_POINT('Ctrl Pts',(-13.2587560588234,-7.31402308269238,
0.254288981130211));
#38392=CARTESIAN_POINT('Ctrl Pts',(-13.2626054360146,-7.30703628683457,
0.342719102199554));
#38393=CARTESIAN_POINT('Ctrl Pts',(-13.2684086950193,-7.29650310602083,
0.476034927301584));
#38394=CARTESIAN_POINT('Ctrl Pts',(-13.2775701666804,-7.27985434187078,
0.608312350205395));
#38395=CARTESIAN_POINT('Ctrl Pts',(-13.2899434176249,-7.25719547792734,
0.739057191237093));
#38396=CARTESIAN_POINT('Ctrl Pts',(-13.3009290370229,-7.23707775329796,
0.855139299993907));
#38397=CARTESIAN_POINT('Ctrl Pts',(-13.3144456587151,-7.21222189770289,
0.970013302477609));
#38398=CARTESIAN_POINT('Ctrl Pts',(-13.3303603014234,-7.18268588222788,
1.08333333333332));
#38399=CARTESIAN_POINT('',(-15.1266902369927,0.68754979644356,1.08333333333333));
#38400=CARTESIAN_POINT('',(-14.2259398250621,0.827729480997533,1.08333333333333));
#38401=CARTESIAN_POINT('Ctrl Pts',(-15.1266902369927,0.687549796443589,
1.08333333333333));
#38402=CARTESIAN_POINT('Ctrl Pts',(-15.0191128271494,0.737684039417719,
1.08333333333333));
#38403=CARTESIAN_POINT('Ctrl Pts',(-14.905210454464,0.775655426636244,1.08333333333333));
#38404=CARTESIAN_POINT('Ctrl Pts',(-14.6232416231909,0.840012972355744,
1.08333333333333));
#38405=CARTESIAN_POINT('Ctrl Pts',(-14.411718162898,0.851428848194329,1.08333333333333));
#38406=CARTESIAN_POINT('Ctrl Pts',(-14.2259398250622,0.827729480996923,
1.08333333333333));
#38407=CARTESIAN_POINT('',(-15.1266902369927,0.687549796443561,-1.08333333333334));
#38408=CARTESIAN_POINT('Ctrl Pts',(-15.1266902369927,0.687549796443564,
1.08333333333333));
#38409=CARTESIAN_POINT('Ctrl Pts',(-15.1249773086751,0.725235701077295,
0.955915065626697));
#38410=CARTESIAN_POINT('Ctrl Pts',(-15.1234319803901,0.756223536825465,
0.826701571450772));
#38411=CARTESIAN_POINT('Ctrl Pts',(-15.122183667988,0.780412301388329,0.696211209492499));
#38412=CARTESIAN_POINT('Ctrl Pts',(-15.1209550316477,0.804219799510246,
0.567777653525797));
#38413=CARTESIAN_POINT('Ctrl Pts',(-15.12001416535,0.821440959530219,0.438107164856512));
#38414=CARTESIAN_POINT('Ctrl Pts',(-15.1194343523859,0.83197783168462,0.307693975181787));
#38415=CARTESIAN_POINT('Ctrl Pts',(-15.1189800281283,0.840234212474348,
0.205506064179395));
#38416=CARTESIAN_POINT('Ctrl Pts',(-15.1187464308798,0.844386527178334,
0.102862147741089));
#38417=CARTESIAN_POINT('Ctrl Pts',(-15.1187464308798,0.844386527178334,
-1.99840144432528E-15));
#38418=CARTESIAN_POINT('Ctrl Pts',(-15.1187464308798,0.844386527178334,
-0.130666807305563));
#38419=CARTESIAN_POINT('Ctrl Pts',(-15.1191251529677,0.837684329050672,
-0.261069786498716));
#38420=CARTESIAN_POINT('Ctrl Pts',(-15.1198518432089,0.824355801783686,
-0.3907104508711));
#38421=CARTESIAN_POINT('Ctrl Pts',(-15.1205872590302,0.810867235029684,
-0.521907748246278));
#38422=CARTESIAN_POINT('Ctrl Pts',(-15.1216790167187,0.790592205023353,
-0.652324314224286));
#38423=CARTESIAN_POINT('Ctrl Pts',(-15.1230415909943,0.763606761086714,
-0.78144348920301));
#38424=CARTESIAN_POINT('Ctrl Pts',(-15.1241128691977,0.742390363261972,
-0.882959098491598));
#38425=CARTESIAN_POINT('Ctrl Pts',(-15.1253504648421,0.717025942629857,
-0.983672743459549));
#38426=CARTESIAN_POINT('Ctrl Pts',(-15.1266902369927,0.687549796443564,
-1.08333333333333));
#38427=CARTESIAN_POINT('',(-14.2259398250711,0.827729480998061,-1.08333333333334));
#38428=CARTESIAN_POINT('Ctrl Pts',(-15.1266902369927,0.687549796443589,
-1.08333333333333));
#38429=CARTESIAN_POINT('Ctrl Pts',(-15.0191128271494,0.73768403941772,-1.08333333333333));
#38430=CARTESIAN_POINT('Ctrl Pts',(-14.905210454464,0.775655426636245,-1.08333333333333));
#38431=CARTESIAN_POINT('Ctrl Pts',(-14.6232416231937,0.840012972355103,
-1.08333333333333));
#38432=CARTESIAN_POINT('Ctrl Pts',(-14.4117181629048,0.851428848194163,
-1.08333333333333));
#38433=CARTESIAN_POINT('Ctrl Pts',(-14.2259398250711,0.827729480998062,
-1.08333333333333));
#38434=CARTESIAN_POINT('Ctrl Pts',(-14.2259398250621,0.827729480996948,
-1.08333333333319));
#38435=CARTESIAN_POINT('Ctrl Pts',(-14.2239464151202,0.86198962338768,-0.949622058007746));
#38436=CARTESIAN_POINT('Ctrl Pts',(-14.2222079250172,0.889808711690097,
-0.814376693553578));
#38437=CARTESIAN_POINT('Ctrl Pts',(-14.2208398148552,0.911161325029729,
-0.678132403728685));
#38438=CARTESIAN_POINT('Ctrl Pts',(-14.2194782068654,0.932412456504284,
-0.542535637671376));
#38439=CARTESIAN_POINT('Ctrl Pts',(-14.2184834780892,0.947258512328182,
-0.405949418799462));
#38440=CARTESIAN_POINT('Ctrl Pts',(-14.2179179597194,0.955671957675903,
-0.268901316712362));
#38441=CARTESIAN_POINT('Ctrl Pts',(-14.2175487034788,0.961165532005871,
-0.179415511019154));
#38442=CARTESIAN_POINT('Ctrl Pts',(-14.2173613909827,0.963916530719958,
-0.0897327832368514));
#38443=CARTESIAN_POINT('Ctrl Pts',(-14.2173613909827,0.963916530719958,
1.77635683940025E-15));
#38444=CARTESIAN_POINT('Ctrl Pts',(-14.2173613909827,0.963916530719959,
0.137573936980362));
#38445=CARTESIAN_POINT('Ctrl Pts',(-14.2178040883167,0.957451598945575,
0.274951212619699));
#38446=CARTESIAN_POINT('Ctrl Pts',(-14.2186598102071,0.944570379379332,
0.411612406214706));
#38447=CARTESIAN_POINT('Ctrl Pts',(-14.2195221530139,0.931589494866292,
0.549330978772852));
#38448=CARTESIAN_POINT('Ctrl Pts',(-14.2208039138492,0.912092599491199,
0.686322345436968));
#38449=CARTESIAN_POINT('Ctrl Pts',(-14.222421741201,0.886126297665223,0.82205493534731));
#38450=CARTESIAN_POINT('Ctrl Pts',(-14.2234666476786,0.869355437073727,
0.909720570537294));
#38451=CARTESIAN_POINT('Ctrl Pts',(-14.2246506698206,0.849885807806941,
0.996861109122796));
#38452=CARTESIAN_POINT('Ctrl Pts',(-14.2259398250621,0.827729480996951,
1.08333333333318));
#38453=CARTESIAN_POINT('Origin',(-13.892722748591,-3.17092330887753,-3.20017169526126E-15));
#38454=CARTESIAN_POINT('',(-13.6476999686241,-6.55970790622096,-1.08333333333334));
#38455=CARTESIAN_POINT('',(-13.1366786991091,-6.483368720524,-1.08333333333334));
#38456=CARTESIAN_POINT('Origin',(-13.892722748591,-3.17092330887753,-1.08333333333334));
#38457=CARTESIAN_POINT('',(-14.6487667980729,0.141522102768936,-1.08333333333334));
#38458=CARTESIAN_POINT('Origin',(-13.892722748591,-3.17092330887753,-3.20017169526126E-15));
#38459=CARTESIAN_POINT('',(-15.1423033840733,-0.0114224867028857,-1.08333333333334));
#38460=CARTESIAN_POINT('Origin',(-13.892722748591,-3.17092330887753,-1.08333333333334));
#38461=CARTESIAN_POINT('',(-15.1423033840733,-0.0114224867028862,1.08333333333333));
#38462=CARTESIAN_POINT('Ctrl Pts',(-15.1423033840733,-0.0114224867028739,
-1.08333333333334));
#38463=CARTESIAN_POINT('Ctrl Pts',(-15.1423953499066,0.110492695607543,
-0.727666221822802));
#38464=CARTESIAN_POINT('Ctrl Pts',(-15.1413590080604,0.169498193350012,
-0.352782973842781));
#38465=CARTESIAN_POINT('Ctrl Pts',(-15.1413590080604,0.169498193350012,
-2.67362166230902E-15));
#38466=CARTESIAN_POINT('Ctrl Pts',(-15.1413590080604,0.169498193350012,
0.352782973842775));
#38467=CARTESIAN_POINT('Ctrl Pts',(-15.1423953499066,0.110492695607543,
0.727666221822795));
#38468=CARTESIAN_POINT('Ctrl Pts',(-15.1423033840733,-0.0114224867028737,
1.08333333333334));
#38469=CARTESIAN_POINT('',(-14.2484814298548,0.20803111085057,1.08333333333333));
#38470=CARTESIAN_POINT('Origin',(-13.892722748591,-3.17092330887754,1.08333333333333));
#38471=CARTESIAN_POINT('',(-14.2484814298548,0.208031110850571,-1.08333333333334));
#38472=CARTESIAN_POINT('Ctrl Pts',(-14.2484814298548,0.208031110850584,
1.08333333333333));
#38473=CARTESIAN_POINT('Ctrl Pts',(-14.2468058395578,0.322795758952019,
0.725928647976579));
#38474=CARTESIAN_POINT('Ctrl Pts',(-14.2449910310593,0.37779693624925,0.352039859176988));
#38475=CARTESIAN_POINT('Ctrl Pts',(-14.2449910310593,0.37779693624925,-2.46631154156404E-15));
#38476=CARTESIAN_POINT('Ctrl Pts',(-14.2449910310593,0.37779693624925,-0.352039859176994));
#38477=CARTESIAN_POINT('Ctrl Pts',(-14.2468058395578,0.322795758952019,
-0.725928647976587));
#38478=CARTESIAN_POINT('Ctrl Pts',(-14.2484814298548,0.208031110850583,
-1.08333333333334));
#38479=CARTESIAN_POINT('Origin',(-13.892722748591,-3.17092330887753,-1.08333333333334));
#38480=CARTESIAN_POINT('',(-12.7471768669563,-6.36961395396413,-1.08333333333334));
#38481=CARTESIAN_POINT('Origin',(-13.892722748591,-3.17092330887753,-1.08333333333334));
#38482=CARTESIAN_POINT('',(-12.7471768669563,-6.36961395396413,1.08333333333333));
#38483=CARTESIAN_POINT('Ctrl Pts',(-12.7471768669563,-6.36961395396412,
-1.08333333333334));
#38484=CARTESIAN_POINT('Ctrl Pts',(-12.6958726976266,-6.472286317656,-0.725928647976585));
#38485=CARTESIAN_POINT('Ctrl Pts',(-12.6703734952066,-6.52105325020167,
-0.352039859176994));
#38486=CARTESIAN_POINT('Ctrl Pts',(-12.6703734952066,-6.52105325020167,
0.352039859176985));
#38487=CARTESIAN_POINT('Ctrl Pts',(-12.6958726976266,-6.472286317656,0.725928647976577));
#38488=CARTESIAN_POINT('Ctrl Pts',(-12.7471768669563,-6.36961395396412,
1.08333333333333));
#38489=CARTESIAN_POINT('',(-13.6476999686241,-6.55970790622096,1.08333333333333));
#38490=CARTESIAN_POINT('Origin',(-13.892722748591,-3.17092330887754,1.08333333333333));
#38491=CARTESIAN_POINT('Ctrl Pts',(-13.6476999686241,-6.55970790622096,
1.08333333333332));
#38492=CARTESIAN_POINT('Ctrl Pts',(-13.5948858118208,-6.66958959248691,
0.727666221822788));
#38493=CARTESIAN_POINT('Ctrl Pts',(-13.5683505740919,-6.72230205711272,
0.35278297384277));
#38494=CARTESIAN_POINT('Ctrl Pts',(-13.5683505740919,-6.72230205711272,
-0.352782973842779));
#38495=CARTESIAN_POINT('Ctrl Pts',(-13.5948858118208,-6.66958959248691,
-0.727666221822796));
#38496=CARTESIAN_POINT('Ctrl Pts',(-13.6476999686241,-6.55970790622096,
-1.08333333333333));
#38497=CARTESIAN_POINT('',(-13.0227870731057,-2.97236616780882,3.45272288248773));
#38498=CARTESIAN_POINT('Origin',(-13.0227870731057,-2.97236616780882,-2.99978307628674E-15));
#38499=CARTESIAN_POINT('',(-14.7626584240763,-3.36948044994625,3.45272288248773));
#38500=CARTESIAN_POINT('Origin',(-14.7626584240763,-3.36948044994625,-3.40056031423578E-15));
#38501=CARTESIAN_POINT('Origin',(-6.18284328242512,-12.8388063676095,-4.97613300162231E-15));
#38502=CARTESIAN_POINT('',(-6.57000108040694,-13.6427478189686,-3.96060240207311));
#38503=CARTESIAN_POINT('Origin',(-6.57000108040694,-13.6427478189686,-5.28772891427451E-15));
#38504=CARTESIAN_POINT('',(-5.79568548444331,-12.0348649162504,-3.96060240207311));
#38505=CARTESIAN_POINT('Origin',(-6.18284328242512,-12.8388063676095,-2.51985201161581));
#38506=CARTESIAN_POINT('Origin',(-5.79568548444331,-12.0348649162504,-4.66453708897012E-15));
#38507=CARTESIAN_POINT('',(-2.35859284151935,-14.0534529496467,1.08333333333333));
#38508=CARTESIAN_POINT('',(-2.69569375163562,-14.9004267538186,1.08333333333333));
#38509=CARTESIAN_POINT('Ctrl Pts',(-2.35859284151934,-14.0534529496467,
1.08333333333333));
#38510=CARTESIAN_POINT('Ctrl Pts',(-2.37682723618162,-14.2398470420046,
1.08333333333333));
#38511=CARTESIAN_POINT('Ctrl Pts',(-2.43502529011671,-14.4435268961719,
1.08333333333332));
#38512=CARTESIAN_POINT('Ctrl Pts',(-2.56051322547963,-14.7041052789647,
1.08333333333333));
#38513=CARTESIAN_POINT('Ctrl Pts',(-2.62287825309305,-14.806702452812,1.08333333333333));
#38514=CARTESIAN_POINT('Ctrl Pts',(-2.69569375163558,-14.9004267538186,
1.08333333333333));
#38515=CARTESIAN_POINT('',(-2.35859284151935,-14.0534529496467,-1.08333333333334));
#38516=CARTESIAN_POINT('Ctrl Pts',(-2.35859284151935,-14.0534529496467,
1.08333333333333));
#38517=CARTESIAN_POINT('Ctrl Pts',(-2.32474809698527,-14.0591331175362,
0.949622058007895));
#38518=CARTESIAN_POINT('Ctrl Pts',(-2.29723964086638,-14.0636285445206,
0.814376693553736));
#38519=CARTESIAN_POINT('Ctrl Pts',(-2.27611794897253,-14.0670461391994,
0.678132403728853));
#38520=CARTESIAN_POINT('Ctrl Pts',(-2.25509664145098,-14.0704474911881,
0.542535637671543));
#38521=CARTESIAN_POINT('Ctrl Pts',(-2.24040145926613,-14.0727812605466,
0.405949418799629));
#38522=CARTESIAN_POINT('Ctrl Pts',(-2.23207311688321,-14.0741020886196,
0.268901316712528));
#38523=CARTESIAN_POINT('Ctrl Pts',(-2.22663511068775,-14.0749645256946,
0.179415511019263));
#38524=CARTESIAN_POINT('Ctrl Pts',(-2.2239114043034,-14.075394064317,0.0897327832369026));
#38525=CARTESIAN_POINT('Ctrl Pts',(-2.2239114043034,-14.075394064317,-8.43769498715119E-15));
#38526=CARTESIAN_POINT('Ctrl Pts',(-2.2239114043034,-14.075394064317,-0.137573936980349));
#38527=CARTESIAN_POINT('Ctrl Pts',(-2.23031275616482,-14.0743870796481,
-0.274951212619667));
#38528=CARTESIAN_POINT('Ctrl Pts',(-2.24306143269717,-14.0723550057958,
-0.411612406214657));
#38529=CARTESIAN_POINT('Ctrl Pts',(-2.25590874866049,-14.0703072093226,
-0.549330978772813));
#38530=CARTESIAN_POINT('Ctrl Pts',(-2.27520203478074,-14.0672183663696,
-0.68632234543694));
#38531=CARTESIAN_POINT('Ctrl Pts',(-2.30087730766032,-14.0630175856782,
-0.822054935347292));
#38532=CARTESIAN_POINT('Ctrl Pts',(-2.31746020132759,-14.0603044266067,
-0.909720570537337));
#38533=CARTESIAN_POINT('Ctrl Pts',(-2.33670515605249,-14.0571263627534,
-0.996861109122898));
#38534=CARTESIAN_POINT('Ctrl Pts',(-2.35859284151935,-14.0534529496467,
-1.08333333333334));
#38535=CARTESIAN_POINT('',(-2.69569375163563,-14.9004267538187,-1.08333333333334));
#38536=CARTESIAN_POINT('Ctrl Pts',(-2.35859284151934,-14.0534529496467,
-1.08333333333333));
#38537=CARTESIAN_POINT('Ctrl Pts',(-2.37688304383397,-14.2404175142851,
-1.08333333333333));
#38538=CARTESIAN_POINT('Ctrl Pts',(-2.43503901504648,-14.4435553962822,
-1.08333333333334));
#38539=CARTESIAN_POINT('Ctrl Pts',(-2.56054033827446,-14.7041615792632,
-1.08333333333334));
#38540=CARTESIAN_POINT('Ctrl Pts',(-2.62284674626764,-14.8066618988743,
-1.08333333333334));
#38541=CARTESIAN_POINT('Ctrl Pts',(-2.69569375163563,-14.9004267538187,
-1.08333333333334));
#38542=CARTESIAN_POINT('Ctrl Pts',(-2.69569375163559,-14.9004267538186,
-1.08333333333335));
#38543=CARTESIAN_POINT('Ctrl Pts',(-2.65857154890325,-14.9071426748862,
-0.955915065626573));
#38544=CARTESIAN_POINT('Ctrl Pts',(-2.628016775001,-14.9125315333598,-0.826701571450498));
#38545=CARTESIAN_POINT('Ctrl Pts',(-2.60415669762586,-14.9166970252376,
-0.696211209492072));
#38546=CARTESIAN_POINT('Ctrl Pts',(-2.58067270588166,-14.9207968600927,
-0.567777653525379));
#38547=CARTESIAN_POINT('Ctrl Pts',(-2.56367395385075,-14.923711651889,-0.438107164856101));
#38548=CARTESIAN_POINT('Ctrl Pts',(-2.55327224255806,-14.9254910506792,
-0.307693975181385));
#38549=CARTESIAN_POINT('Ctrl Pts',(-2.54512176981446,-14.9268853348437,
-0.205506064179128));
#38550=CARTESIAN_POINT('Ctrl Pts',(-2.54102158203148,-14.9275815713119,
-0.102862147740959));
#38551=CARTESIAN_POINT('Ctrl Pts',(-2.54102158203148,-14.9275815713119,
-4.44089209850063E-15));
#38552=CARTESIAN_POINT('Ctrl Pts',(-2.54102158203148,-14.9275815713119,
0.130666807305524));
#38553=CARTESIAN_POINT('Ctrl Pts',(-2.54764001565181,-14.9264594186595,
0.261069786498646));
#38554=CARTESIAN_POINT('Ctrl Pts',(-2.56079607270382,-14.9242020129234,
0.390710450870999));
#38555=CARTESIAN_POINT('Ctrl Pts',(-2.57411009834303,-14.9219175018628,
0.521907748246163));
#38556=CARTESIAN_POINT('Ctrl Pts',(-2.59411972995703,-14.9184702682937,
0.652324314224157));
#38557=CARTESIAN_POINT('Ctrl Pts',(-2.62073179377387,-14.9137938537994,
0.781443489202868));
#38558=CARTESIAN_POINT('Ctrl Pts',(-2.64165463403551,-14.9101171801624,
0.882959098491507));
#38559=CARTESIAN_POINT('Ctrl Pts',(-2.66665850662476,-14.9056796321318,
0.983672743459509));
#38560=CARTESIAN_POINT('Ctrl Pts',(-2.69569375163559,-14.9004267538186,
1.08333333333334));
#38561=CARTESIAN_POINT('',(-9.96888517526507,-11.3978423664701,1.08333333333333));
#38562=CARTESIAN_POINT('',(-9.516873369993,-10.6062067328295,1.08333333333333));
#38563=CARTESIAN_POINT('Ctrl Pts',(-9.96888517526507,-11.3978423664701,
1.08333333333333));
#38564=CARTESIAN_POINT('Ctrl Pts',(-9.94100828682427,-11.282476771434,1.08333333333333));
#38565=CARTESIAN_POINT('Ctrl Pts',(-9.89967854500783,-11.1697495378475,
1.08333333333333));
#38566=CARTESIAN_POINT('Ctrl Pts',(-9.77419060964491,-10.9091711550547,
1.08333333333333));
#38567=CARTESIAN_POINT('Ctrl Pts',(-9.65123318042897,-10.7366777723525,
1.08333333333333));
#38568=CARTESIAN_POINT('Ctrl Pts',(-9.51687336999256,-10.6062067328299,
1.08333333333333));
#38569=CARTESIAN_POINT('',(-9.96888517526507,-11.3978423664701,-1.08333333333334));
#38570=CARTESIAN_POINT('Ctrl Pts',(-9.96888517526508,-11.3978423664701,
1.08333333333333));
#38571=CARTESIAN_POINT('Ctrl Pts',(-9.99706424266063,-11.3731961327199,
0.956888632103256));
#38572=CARTESIAN_POINT('Ctrl Pts',(-10.020155672713,-11.3528209383891,0.828820583351071));
#38573=CARTESIAN_POINT('Ctrl Pts',(-10.038197564346,-11.3368457653652,0.699646919261599));
#38574=CARTESIAN_POINT('Ctrl Pts',(-10.0561445912219,-11.3209545902358,
0.571152453812953));
#38575=CARTESIAN_POINT('Ctrl Pts',(-10.0690951385517,-11.3094172714603,
0.441563969171296));
#38576=CARTESIAN_POINT('Ctrl Pts',(-10.0770534136919,-11.3023217413999,
0.311391073637437));
#38577=CARTESIAN_POINT('Ctrl Pts',(-10.0849478229272,-11.2952831536342,
0.182262827807044));
#38578=CARTESIAN_POINT('Ctrl Pts',(-10.0879298097314,-11.2926153440655,
0.0525595133516554));
#38579=CARTESIAN_POINT('Ctrl Pts',(-10.0859696068728,-11.2943658227348,
-0.0772214321950453));
#38580=CARTESIAN_POINT('Ctrl Pts',(-10.0846326712896,-11.2955597181575,
-0.165737150534751));
#38581=CARTESIAN_POINT('Ctrl Pts',(-10.0809960349672,-11.2988081152181,
-0.2542889811304));
#38582=CARTESIAN_POINT('Ctrl Pts',(-10.0750409796764,-11.304115688826,-0.342719102199531));
#38583=CARTESIAN_POINT('Ctrl Pts',(-10.0660632343107,-11.3121173012435,
-0.476034927301883));
#38584=CARTESIAN_POINT('Ctrl Pts',(-10.0518705086679,-11.3247537742305,
-0.608312350206005));
#38585=CARTESIAN_POINT('Ctrl Pts',(-10.0325330571073,-11.3418588735079,
-0.739057191238004));
#38586=CARTESIAN_POINT('Ctrl Pts',(-10.0153642561251,-11.3570456753652,
-0.855139299994515));
#38587=CARTESIAN_POINT('Ctrl Pts',(-9.99413932000721,-11.3757543553326,
-0.970013302477919));
#38588=CARTESIAN_POINT('Ctrl Pts',(-9.96888517526508,-11.3978423664701,
-1.08333333333334));
#38589=CARTESIAN_POINT('',(-9.51687336999906,-10.6062067328363,-1.08333333333334));
#38590=CARTESIAN_POINT('Ctrl Pts',(-9.96888517526507,-11.3978423664701,
-1.08333333333333));
#38591=CARTESIAN_POINT('Ctrl Pts',(-9.94100828682427,-11.282476771434,-1.08333333333333));
#38592=CARTESIAN_POINT('Ctrl Pts',(-9.89967854500783,-11.1697495378475,
-1.08333333333333));
#38593=CARTESIAN_POINT('Ctrl Pts',(-9.77419060964618,-10.9091711550573,
-1.08333333333333));
#38594=CARTESIAN_POINT('Ctrl Pts',(-9.6512331804331,-10.7366777723579,-1.08333333333333));
#38595=CARTESIAN_POINT('Ctrl Pts',(-9.51687336999908,-10.6062067328363,
-1.08333333333333));
#38596=CARTESIAN_POINT('Ctrl Pts',(-9.51687336999256,-10.6062067328299,
-1.08333333333319));
#38597=CARTESIAN_POINT('Ctrl Pts',(-9.54248335115827,-10.5832270800755,
-0.949270311030248));
#38598=CARTESIAN_POINT('Ctrl Pts',(-9.56321910180067,-10.5644593135702,
-0.813521288367661));
#38599=CARTESIAN_POINT('Ctrl Pts',(-9.57910097474595,-10.5500390764974,
-0.676607052100613));
#38600=CARTESIAN_POINT('Ctrl Pts',(-9.59267821366648,-10.5377113740467,
-0.559560573777554));
#38601=CARTESIAN_POINT('Ctrl Pts',(-9.6027075928823,-10.5285603838747,-0.44166251627891));
#38602=CARTESIAN_POINT('Ctrl Pts',(-9.6091818848891,-10.5226481221753,-0.323238258334718));
#38603=CARTESIAN_POINT('Ctrl Pts',(-9.61666296645239,-10.5158164698571,
-0.186398348762648));
#38604=CARTESIAN_POINT('Ctrl Pts',(-9.61937600851194,-10.5133302394117,
-0.0492519096262118));
#38605=CARTESIAN_POINT('Ctrl Pts',(-9.61735300288125,-10.5151805128572,
0.08767582706605));
#38606=CARTESIAN_POINT('Ctrl Pts',(-9.61532413250719,-10.5170361502911,
0.225000520654331));
#38607=CARTESIAN_POINT('Ctrl Pts',(-9.60853168799772,-10.5232534570122,
0.362105241912796));
#38608=CARTESIAN_POINT('Ctrl Pts',(-9.59697252030892,-10.5337846211338,
0.498460177595657));
#38609=CARTESIAN_POINT('Ctrl Pts',(-9.5853634847053,-10.5443612182148,0.635403368116659));
#38610=CARTESIAN_POINT('Ctrl Pts',(-9.56894645381043,-10.5592890006364,
0.771590289741169));
#38611=CARTESIAN_POINT('Ctrl Pts',(-9.54768316346852,-10.578480335569,0.906484242526434));
#38612=CARTESIAN_POINT('Ctrl Pts',(-9.53834928383367,-10.5869046954593,
0.965698216399696));
#38613=CARTESIAN_POINT('Ctrl Pts',(-9.52808112091929,-10.5961500981613,
1.02466304565381));
#38614=CARTESIAN_POINT('Ctrl Pts',(-9.51687336999256,-10.6062067328299,
1.08333333333318));
#38615=CARTESIAN_POINT('Origin',(-6.18284328242512,-12.8388063676095,-4.97613300162231E-15));
#38616=CARTESIAN_POINT('',(-3.38061559238688,-14.7601124814492,-1.08333333333334));
#38617=CARTESIAN_POINT('',(-3.12168342103518,-14.3129832609672,-1.08333333333334));
#38618=CARTESIAN_POINT('Origin',(-6.18284328242512,-12.8388063676095,-1.08333333333334));
#38619=CARTESIAN_POINT('',(-9.24400314381506,-11.3646294742518,-1.08333333333334));
#38620=CARTESIAN_POINT('Origin',(-6.18284328242512,-12.8388063676095,-4.97613300162231E-15));
#38621=CARTESIAN_POINT('',(-9.43214127690829,-11.8458513067218,-1.08333333333334));
#38622=CARTESIAN_POINT('Origin',(-6.18284328242512,-12.8388063676095,-1.08333333333334));
#38623=CARTESIAN_POINT('',(-9.43214127690829,-11.8458513067218,1.08333333333333));
#38624=CARTESIAN_POINT('Ctrl Pts',(-9.43214127690829,-11.8458513067218,
-1.08333333333333));
#38625=CARTESIAN_POINT('Ctrl Pts',(-9.52751574438859,-11.7699103356433,
-0.727666221822795));
#38626=CARTESIAN_POINT('Ctrl Pts',(-9.57300195158999,-11.7323107648653,
-0.352782973842778));
#38627=CARTESIAN_POINT('Ctrl Pts',(-9.57300195158999,-11.7323107648653,
-4.85994849902029E-15));
#38628=CARTESIAN_POINT('Ctrl Pts',(-9.57300195158999,-11.7323107648653,
0.352782973842767));
#38629=CARTESIAN_POINT('Ctrl Pts',(-9.52751574438859,-11.7699103356433,
0.727666221822782));
#38630=CARTESIAN_POINT('Ctrl Pts',(-9.43214127690829,-11.8458513067218,
1.08333333333332));
#38631=CARTESIAN_POINT('',(-9.04642813528379,-11.0102060831369,1.08333333333333));
#38632=CARTESIAN_POINT('Origin',(-6.18284328242512,-12.8388063676095,1.08333333333333));
#38633=CARTESIAN_POINT('',(-9.04642813528379,-11.0102060831369,-1.08333333333334));
#38634=CARTESIAN_POINT('Ctrl Pts',(-9.0464281352838,-11.0102060831369,1.08333333333332));
#38635=CARTESIAN_POINT('Ctrl Pts',(-9.13511003678158,-10.9373414661859,
0.725928647976571));
#38636=CARTESIAN_POINT('Ctrl Pts',(-9.17698017417422,-10.901629918632,0.352039859176983));
#38637=CARTESIAN_POINT('Ctrl Pts',(-9.17698017417422,-10.901629918632,-4.5383086406711E-15));
#38638=CARTESIAN_POINT('Ctrl Pts',(-9.17698017417422,-10.901629918632,-0.352039859176993));
#38639=CARTESIAN_POINT('Ctrl Pts',(-9.13511003678158,-10.9373414661859,
-0.725928647976581));
#38640=CARTESIAN_POINT('Ctrl Pts',(-9.0464281352838,-11.0102060831369,-1.08333333333333));
#38641=CARTESIAN_POINT('Origin',(-6.18284328242512,-12.8388063676095,-1.08333333333334));
#38642=CARTESIAN_POINT('',(-2.96777005865995,-13.9375335292483,-1.08333333333334));
#38643=CARTESIAN_POINT('Origin',(-6.18284328242512,-12.8388063676095,-1.08333333333334));
#38644=CARTESIAN_POINT('',(-2.96777005865995,-13.9375335292483,1.08333333333333));
#38645=CARTESIAN_POINT('Ctrl Pts',(-2.96777005865994,-13.9375335292483,
-1.08333333333334));
#38646=CARTESIAN_POINT('Ctrl Pts',(-2.85550994597631,-13.9614374861791,
-0.725928647976589));
#38647=CARTESIAN_POINT('Ctrl Pts',(-2.80148393014434,-13.9719070920595,
-0.352039859176996));
#38648=CARTESIAN_POINT('Ctrl Pts',(-2.80148393014434,-13.9719070920595,
0.352039859176986));
#38649=CARTESIAN_POINT('Ctrl Pts',(-2.85550994597631,-13.9614374861791,
0.725928647976578));
#38650=CARTESIAN_POINT('Ctrl Pts',(-2.96777005865994,-13.9375335292483,
1.08333333333333));
#38651=CARTESIAN_POINT('',(-3.38061559238688,-14.7601124814492,1.08333333333333));
#38652=CARTESIAN_POINT('Origin',(-6.18284328242512,-12.8388063676095,1.08333333333333));
#38653=CARTESIAN_POINT('Ctrl Pts',(-3.38061559238688,-14.7601124814492,
1.08333333333333));
#38654=CARTESIAN_POINT('Ctrl Pts',(-3.26177754255684,-14.7873308217382,
0.727666221822789));
#38655=CARTESIAN_POINT('Ctrl Pts',(-3.20402082808,-14.799450421612,0.35278297384277));
#38656=CARTESIAN_POINT('Ctrl Pts',(-3.20402082808,-14.799450421612,-0.352782973842781));
#38657=CARTESIAN_POINT('Ctrl Pts',(-3.26177754255684,-14.7873308217382,
-0.727666221822799));
#38658=CARTESIAN_POINT('Ctrl Pts',(-3.38061559238688,-14.7601124814492,
-1.08333333333334));
#38659=CARTESIAN_POINT('',(-5.79568548444331,-12.0348649162504,3.45272288248773));
#38660=CARTESIAN_POINT('Origin',(-5.79568548444331,-12.0348649162504,-4.66453708897012E-15));
#38661=CARTESIAN_POINT('',(-6.57000108040694,-13.6427478189686,3.45272288248772));
#38662=CARTESIAN_POINT('Origin',(-6.57000108040694,-13.6427478189686,-5.28772891427451E-15));
#38663=CARTESIAN_POINT('Origin',(6.1828432824253,-12.8388063676094,-4.9761330016223E-15));
#38664=CARTESIAN_POINT('',(6.57000108040713,-13.6427478189685,-3.96060240207311));
#38665=CARTESIAN_POINT('Origin',(6.57000108040713,-13.6427478189685,-5.28772891427449E-15));
#38666=CARTESIAN_POINT('',(5.79568548444348,-12.0348649162503,-3.96060240207311));
#38667=CARTESIAN_POINT('Origin',(6.1828432824253,-12.8388063676094,-2.51985201161581));
#38668=CARTESIAN_POINT('Origin',(5.79568548444348,-12.0348649162504,-4.66453708897011E-15));
#38669=CARTESIAN_POINT('',(9.51687336999268,-10.6062067328298,1.08333333333333));
#38670=CARTESIAN_POINT('',(9.96888517526453,-11.3978423664706,1.08333333333333));
#38671=CARTESIAN_POINT('Ctrl Pts',(9.5168733699927,-10.6062067328298,1.08333333333333));
#38672=CARTESIAN_POINT('Ctrl Pts',(9.65164439811578,-10.737077088181,1.08333333333333));
#38673=CARTESIAN_POINT('Ctrl Pts',(9.77420433457484,-10.9091996551649,1.08333333333333));
#38674=CARTESIAN_POINT('Ctrl Pts',(9.89970565780286,-11.169805838146,1.08333333333333));
#38675=CARTESIAN_POINT('Ctrl Pts',(9.94099622466366,-11.2824268534395,1.08333333333333));
#38676=CARTESIAN_POINT('Ctrl Pts',(9.96888517526534,-11.3978423664704,1.08333333333333));
#38677=CARTESIAN_POINT('',(9.51687336999268,-10.6062067328298,-1.08333333333334));
#38678=CARTESIAN_POINT('Ctrl Pts',(9.51687336999268,-10.6062067328298,1.08333333333333));
#38679=CARTESIAN_POINT('Ctrl Pts',(9.54241615713793,-10.5832873727889,0.949622058007762));
#38680=CARTESIAN_POINT('Ctrl Pts',(9.56308206533645,-10.5645832486408,0.814376693553466));
#38681=CARTESIAN_POINT('Ctrl Pts',(9.5789232079445,-10.5502004803844,0.678132403728444));
#38682=CARTESIAN_POINT('Ctrl Pts',(9.59468906287363,-10.5358860686389,0.542535637671145));
#38683=CARTESIAN_POINT('Ctrl Pts',(9.60567597345963,-10.5258519939611,0.405949418799242));
#38684=CARTESIAN_POINT('Ctrl Pts',(9.61190127497217,-10.5201641565229,0.268901316712153));
#38685=CARTESIAN_POINT('Ctrl Pts',(9.61596609683434,-10.5164502727984,0.179415511019018));
#38686=CARTESIAN_POINT('Ctrl Pts',(9.61800012680612,-10.5145886063487,0.0897327832367887));
#38687=CARTESIAN_POINT('Ctrl Pts',(9.61800012680612,-10.5145886063487,9.32587340685131E-15));
#38688=CARTESIAN_POINT('Ctrl Pts',(9.61800012680612,-10.5145886063487,-0.137573936980381));
#38689=CARTESIAN_POINT('Ctrl Pts',(9.61322165688595,-10.5189655400926,-0.274951212619743));
#38690=CARTESIAN_POINT('Ctrl Pts',(9.6036842477684,-10.5276658794419,-0.411612406214774));
#38691=CARTESIAN_POINT('Ctrl Pts',(9.59407304553156,-10.5364335353099,-0.54933097877281));
#38692=CARTESIAN_POINT('Ctrl Pts',(9.57962892372621,-10.5495917717182,-0.686322345436814));
#38693=CARTESIAN_POINT('Ctrl Pts',(9.5603363503304,-10.5670463644555,-0.822054935347047));
#38694=CARTESIAN_POINT('Ctrl Pts',(9.54787585206456,-10.5783197657831,-0.909720570537174));
#38695=CARTESIAN_POINT('Ctrl Pts',(9.5333921086825,-10.5913845868635,-0.996861109122817));
#38696=CARTESIAN_POINT('Ctrl Pts',(9.51687336999268,-10.6062067328298,-1.08333333333334));
#38697=CARTESIAN_POINT('',(9.9688851752657,-11.3978423664719,-1.08333333333334));
#38698=CARTESIAN_POINT('Ctrl Pts',(9.5168733699927,-10.6062067328298,-1.08333333333333));
#38699=CARTESIAN_POINT('Ctrl Pts',(9.65123318042911,-10.7366777723523,-1.08333333333333));
#38700=CARTESIAN_POINT('Ctrl Pts',(9.77419060964506,-10.9091711550545,-1.08333333333333));
#38701=CARTESIAN_POINT('Ctrl Pts',(9.89967854500826,-11.1697495378479,-1.08333333333333));
#38702=CARTESIAN_POINT('Ctrl Pts',(9.94100828682489,-11.2824767714351,-1.08333333333333));
#38703=CARTESIAN_POINT('Ctrl Pts',(9.96888517526571,-11.3978423664719,-1.08333333333333));
#38704=CARTESIAN_POINT('Ctrl Pts',(9.96888517526519,-11.39784236647,-1.08333333333359));
#38705=CARTESIAN_POINT('Ctrl Pts',(9.99728120861575,-11.3730063679711,-0.955915065626921));
#38706=CARTESIAN_POINT('Ctrl Pts',(10.0205449777511,-11.3524775820965,-0.826701571450959));
#38707=CARTESIAN_POINT('Ctrl Pts',(10.038678205356,-11.3364201641361,-0.696211209492648));
#38708=CARTESIAN_POINT('Ctrl Pts',(10.0565256146782,-11.3206158452779,-0.567777653525928));
#38709=CARTESIAN_POINT('Ctrl Pts',(10.0694030392049,-11.309143028737,-0.438107164856624));
#38710=CARTESIAN_POINT('Ctrl Pts',(10.0772795901119,-11.3021200803759,-0.307693975181881));
#38711=CARTESIAN_POINT('Ctrl Pts',(10.0834514220032,-11.2966171061454,-0.20550606417946));
#38712=CARTESIAN_POINT('Ctrl Pts',(10.0865521868617,-11.2938455465903,-0.102862147741125));
#38713=CARTESIAN_POINT('Ctrl Pts',(10.0865521868617,-11.2938455465903,-4.44089209850063E-15));
#38714=CARTESIAN_POINT('Ctrl Pts',(10.0865521868617,-11.2938455465903,0.130666807305562));
#38715=CARTESIAN_POINT('Ctrl Pts',(10.0815483267233,-11.2983203956244,0.261069786498721));
#38716=CARTESIAN_POINT('Ctrl Pts',(10.0715807484455,-11.3071987457576,0.390710450871112));
#38717=CARTESIAN_POINT('Ctrl Pts',(10.0614934865685,-11.3161837008123,0.521907748246463));
#38718=CARTESIAN_POINT('Ctrl Pts',(10.0463225295865,-11.3296785457857,0.652324314224642));
#38719=CARTESIAN_POINT('Ctrl Pts',(10.0260740111135,-11.3475689983448,0.781443489203535));
#38720=CARTESIAN_POINT('Ctrl Pts',(10.0101542943843,-11.3616347650465,0.88295909849203));
#38721=CARTESIAN_POINT('Ctrl Pts',(9.99109522006272,-11.3784168138781,0.983672743459888));
#38722=CARTESIAN_POINT('Ctrl Pts',(9.96888517526519,-11.39784236647,1.08333333333358));
#38723=CARTESIAN_POINT('',(2.69569375163578,-14.9004267538186,1.08333333333333));
#38724=CARTESIAN_POINT('',(2.35859284151893,-14.0534529496468,1.08333333333333));
#38725=CARTESIAN_POINT('Ctrl Pts',(2.6956937516358,-14.9004267538186,1.08333333333332));
#38726=CARTESIAN_POINT('Ctrl Pts',(2.62284674626782,-14.8066618988742,1.08333333333332));
#38727=CARTESIAN_POINT('Ctrl Pts',(2.56054033827465,-14.7041615792632,1.08333333333332));
#38728=CARTESIAN_POINT('Ctrl Pts',(2.4350390150467,-14.4435553962822,1.08333333333332));
#38729=CARTESIAN_POINT('Ctrl Pts',(2.37688304383419,-14.2404175142851,1.08333333333332));
#38730=CARTESIAN_POINT('Ctrl Pts',(2.35859284151955,-14.0534529496467,1.08333333333332));
#38731=CARTESIAN_POINT('',(2.69569375163578,-14.9004267538186,-1.08333333333334));
#38732=CARTESIAN_POINT('Ctrl Pts',(2.69569375163578,-14.9004267538186,1.08333333333333));
#38733=CARTESIAN_POINT('Ctrl Pts',(2.65885518901859,-14.9070913604575,0.956888632103347));
#38734=CARTESIAN_POINT('Ctrl Pts',(2.62852794948137,-14.9124412415715,0.828820583351256));
#38735=CARTESIAN_POINT('Ctrl Pts',(2.60478912083403,-14.9165866029902,0.699646919261879));
#38736=CARTESIAN_POINT('Ctrl Pts',(2.58117511159368,-14.9207101679857,0.571152453813268));
#38737=CARTESIAN_POINT('Ctrl Pts',(2.56408033836306,-14.9236419130061,0.441563969171648));
#38738=CARTESIAN_POINT('Ctrl Pts',(2.55357092618676,-14.9254399524253,0.311391073637824));
#38739=CARTESIAN_POINT('Ctrl Pts',(2.54314585302948,-14.9272235624095,0.182262827807427));
#38740=CARTESIAN_POINT('Ctrl Pts',(2.53920083715778,-14.927891621514,0.0525595133520343));
#38741=CARTESIAN_POINT('Ctrl Pts',(2.54179158298272,-14.9274504788058,-0.077221432194672));
#38742=CARTESIAN_POINT('Ctrl Pts',(2.54355857371286,-14.9271496020974,-0.165737150534507));
#38743=CARTESIAN_POINT('Ctrl Pts',(2.54836567846244,-14.9263317077699,-0.254288981130285));
#38744=CARTESIAN_POINT('Ctrl Pts',(2.55622822284789,-14.9249850760809,-0.342719102199546));
#38745=CARTESIAN_POINT('Ctrl Pts',(2.56808166802554,-14.9229549158531,-0.47603492730158));
#38746=CARTESIAN_POINT('Ctrl Pts',(2.58681028013297,-14.9197373081624,-0.608312350205393));
#38747=CARTESIAN_POINT('Ctrl Pts',(2.61224028910069,-14.9152835347009,-0.739057191237091));
#38748=CARTESIAN_POINT('Ctrl Pts',(2.63481838123332,-14.9113292416576,-0.855139299993913));
#38749=CARTESIAN_POINT('Ctrl Pts',(2.66267894744191,-14.9063995895532,-0.970013302477622));
#38750=CARTESIAN_POINT('Ctrl Pts',(2.69569375163578,-14.9004267538186,-1.08333333333334));
#38751=CARTESIAN_POINT('',(2.35859284152043,-14.0534529496557,-1.08333333333334));
#38752=CARTESIAN_POINT('Ctrl Pts',(2.6956937516358,-14.9004267538186,-1.08333333333334));
#38753=CARTESIAN_POINT('Ctrl Pts',(2.62284674626782,-14.8066618988742,-1.08333333333334));
#38754=CARTESIAN_POINT('Ctrl Pts',(2.56054033827465,-14.7041615792632,-1.08333333333334));
#38755=CARTESIAN_POINT('Ctrl Pts',(2.43503901504795,-14.4435553962848,-1.08333333333334));
#38756=CARTESIAN_POINT('Ctrl Pts',(2.37688304383586,-14.2404175142916,-1.08333333333334));
#38757=CARTESIAN_POINT('Ctrl Pts',(2.35859284152042,-14.0534529496557,-1.08333333333334));
#38758=CARTESIAN_POINT('Ctrl Pts',(2.35859284151951,-14.0534529496467,-1.08333333333319));
#38759=CARTESIAN_POINT('Ctrl Pts',(2.32465906345733,-14.0591480600448,-0.949270311030372));
#38760=CARTESIAN_POINT('Ctrl Pts',(2.29705730368849,-14.0636584116899,-0.813521288367913));
#38761=CARTESIAN_POINT('Ctrl Pts',(2.27588092254449,-14.0670844892038,-0.676607052100994));
#38762=CARTESIAN_POINT('Ctrl Pts',(2.25777746665768,-14.0700134052785,-0.55956057377781));
#38763=CARTESIAN_POINT('Ctrl Pts',(2.24436971878542,-14.0721491406499,-0.441662516279038));
#38764=CARTESIAN_POINT('Ctrl Pts',(2.23571067141573,-14.073524711092,-0.323238258334718));
#38765=CARTESIAN_POINT('Ctrl Pts',(2.2257050924945,-14.0751141906309,-0.186398348762649));
#38766=CARTESIAN_POINT('Ctrl Pts',(2.22206972520347,-14.0756851929985,-0.0492519096262131));
#38767=CARTESIAN_POINT('Ctrl Pts',(2.22477765061414,-14.0752571701311,0.087675827066048));
#38768=CARTESIAN_POINT('Ctrl Pts',(2.22749342636756,-14.0748279064149,0.225000520654297));
#38769=CARTESIAN_POINT('Ctrl Pts',(2.23658933237962,-14.0733937867901,0.362105241912729));
#38770=CARTESIAN_POINT('Ctrl Pts',(2.25202995120888,-14.0709225390114,0.498460177595558));
#38771=CARTESIAN_POINT('Ctrl Pts',(2.26753718309241,-14.0684406299137,0.635403368116538));
#38772=CARTESIAN_POINT('Ctrl Pts',(2.28944404469282,-14.0649125984157,0.771590289741026));
#38773=CARTESIAN_POINT('Ctrl Pts',(2.31770587921582,-14.0602538902201,0.906484242526269));
#38774=CARTESIAN_POINT('Ctrl Pts',(2.33011188776182,-14.0582088717468,0.965698216399587));
#38775=CARTESIAN_POINT('Ctrl Pts',(2.34374232952329,-14.0559453130119,1.02466304565376));
#38776=CARTESIAN_POINT('Ctrl Pts',(2.35859284151951,-14.0534529496467,1.08333333333318));
#38777=CARTESIAN_POINT('Origin',(6.1828432824253,-12.8388063676094,-4.9761330016223E-15));
#38778=CARTESIAN_POINT('',(9.43214127690845,-11.8458513067217,-1.08333333333334));
#38779=CARTESIAN_POINT('',(9.24400314381522,-11.3646294742516,-1.08333333333334));
#38780=CARTESIAN_POINT('Origin',(6.1828432824253,-12.8388063676094,-1.08333333333334));
#38781=CARTESIAN_POINT('',(3.12168342103538,-14.3129832609672,-1.08333333333334));
#38782=CARTESIAN_POINT('Origin',(6.1828432824253,-12.8388063676094,-4.9761330016223E-15));
#38783=CARTESIAN_POINT('',(3.38061559238708,-14.7601124814491,-1.08333333333334));
#38784=CARTESIAN_POINT('Origin',(6.1828432824253,-12.8388063676094,-1.08333333333334));
#38785=CARTESIAN_POINT('',(3.38061559238708,-14.7601124814491,1.08333333333333));
#38786=CARTESIAN_POINT('Ctrl Pts',(3.3806155923871,-14.7601124814491,-1.08333333333334));
#38787=CARTESIAN_POINT('Ctrl Pts',(3.26177754255705,-14.7873308217381,-0.7276662218228));
#38788=CARTESIAN_POINT('Ctrl Pts',(3.20402082808022,-14.7994504216119,-0.35278297384278));
#38789=CARTESIAN_POINT('Ctrl Pts',(3.20402082808022,-14.7994504216119,-5.42337291349619E-15));
#38790=CARTESIAN_POINT('Ctrl Pts',(3.20402082808022,-14.7994504216119,0.352782973842771));
#38791=CARTESIAN_POINT('Ctrl Pts',(3.26177754255705,-14.7873308217381,0.727666221822789));
#38792=CARTESIAN_POINT('Ctrl Pts',(3.3806155923871,-14.7601124814491,1.08333333333333));
#38793=CARTESIAN_POINT('',(2.96777005866014,-13.9375335292483,1.08333333333333));
#38794=CARTESIAN_POINT('Origin',(6.1828432824253,-12.8388063676094,1.08333333333333));
#38795=CARTESIAN_POINT('',(2.96777005866014,-13.9375335292483,-1.08333333333334));
#38796=CARTESIAN_POINT('Ctrl Pts',(2.96777005866014,-13.9375335292483,1.08333333333333));
#38797=CARTESIAN_POINT('Ctrl Pts',(2.85550994597651,-13.9614374861791,0.725928647976575));
#38798=CARTESIAN_POINT('Ctrl Pts',(2.80148393014454,-13.9719070920595,0.352039859176984));
#38799=CARTESIAN_POINT('Ctrl Pts',(2.80148393014454,-13.9719070920595,-5.10230940761107E-15));
#38800=CARTESIAN_POINT('Ctrl Pts',(2.80148393014454,-13.9719070920595,-0.352039859176994));
#38801=CARTESIAN_POINT('Ctrl Pts',(2.85550994597651,-13.9614374861791,-0.725928647976584));
#38802=CARTESIAN_POINT('Ctrl Pts',(2.96777005866014,-13.9375335292483,-1.08333333333334));
#38803=CARTESIAN_POINT('Origin',(6.1828432824253,-12.8388063676094,-1.08333333333334));
#38804=CARTESIAN_POINT('',(9.04642813528394,-11.0102060831368,-1.08333333333334));
#38805=CARTESIAN_POINT('Origin',(6.1828432824253,-12.8388063676094,-1.08333333333334));
#38806=CARTESIAN_POINT('',(9.04642813528394,-11.0102060831368,1.08333333333333));
#38807=CARTESIAN_POINT('Ctrl Pts',(9.04642813528395,-11.0102060831368,-1.08333333333334));
#38808=CARTESIAN_POINT('Ctrl Pts',(9.13511003678174,-10.9373414661857,-0.725928647976586));
#38809=CARTESIAN_POINT('Ctrl Pts',(9.17698017417438,-10.9016299186319,-0.352039859176995));
#38810=CARTESIAN_POINT('Ctrl Pts',(9.17698017417438,-10.9016299186319,0.352039859176985));
#38811=CARTESIAN_POINT('Ctrl Pts',(9.13511003678174,-10.9373414661857,0.725928647976577));
#38812=CARTESIAN_POINT('Ctrl Pts',(9.04642813528396,-11.0102060831368,1.08333333333333));
#38813=CARTESIAN_POINT('',(9.43214127690845,-11.8458513067217,1.08333333333333));
#38814=CARTESIAN_POINT('Origin',(6.1828432824253,-12.8388063676094,1.08333333333333));
#38815=CARTESIAN_POINT('Ctrl Pts',(9.43214127690846,-11.8458513067217,1.08333333333333));
#38816=CARTESIAN_POINT('Ctrl Pts',(9.52751574438876,-11.7699103356432,0.727666221822791));
#38817=CARTESIAN_POINT('Ctrl Pts',(9.57300195159016,-11.7323107648652,0.352782973842771));
#38818=CARTESIAN_POINT('Ctrl Pts',(9.57300195159016,-11.7323107648652,-0.352782973842781));
#38819=CARTESIAN_POINT('Ctrl Pts',(9.52751574438875,-11.7699103356432,-0.7276662218228));
#38820=CARTESIAN_POINT('Ctrl Pts',(9.43214127690846,-11.8458513067217,-1.08333333333334));
#38821=CARTESIAN_POINT('',(5.79568548444348,-12.0348649162504,3.45272288248773));
#38822=CARTESIAN_POINT('Origin',(5.79568548444348,-12.0348649162504,-4.66453708897011E-15));
#38823=CARTESIAN_POINT('',(6.57000108040713,-13.6427478189685,3.45272288248772));
#38824=CARTESIAN_POINT('Origin',(6.57000108040713,-13.6427478189685,-5.28772891427449E-15));
#38825=CARTESIAN_POINT('Origin',(13.892722748591,-3.17092330887735,-3.20017169526122E-15));
#38826=CARTESIAN_POINT('',(14.7626584240763,-3.36948044994605,-3.96060240207311));
#38827=CARTESIAN_POINT('Origin',(14.7626584240763,-3.36948044994605,-3.40056031423575E-15));
#38828=CARTESIAN_POINT('',(13.0227870731057,-2.97236616780864,-3.96060240207311));
#38829=CARTESIAN_POINT('Origin',(13.892722748591,-3.17092330887735,-2.5198520116158));
#38830=CARTESIAN_POINT('Origin',(13.0227870731057,-2.97236616780865,-2.9997830762867E-15));
#38831=CARTESIAN_POINT('',(14.2259398250621,0.827729480997053,1.08333333333333));
#38832=CARTESIAN_POINT('',(15.1266902369927,0.68754979644376,1.08333333333333));
#38833=CARTESIAN_POINT('Ctrl Pts',(14.2259398250621,0.827729480997104,1.08333333333333));
#38834=CARTESIAN_POINT('Ctrl Pts',(14.4122867506183,0.85150138178118,1.08333333333333));
#38835=CARTESIAN_POINT('Ctrl Pts',(14.6232724628281,0.840005933409976,1.08333333333333));
#38836=CARTESIAN_POINT('Ctrl Pts',(14.9052713763609,0.775641521611009,1.08333333333333));
#38837=CARTESIAN_POINT('Ctrl Pts',(15.0190662790554,0.737705732201359,1.08333333333333));
#38838=CARTESIAN_POINT('Ctrl Pts',(15.1266902369927,0.687549796443767,1.08333333333333));
#38839=CARTESIAN_POINT('',(14.2259398250621,0.827729480997055,-1.08333333333334));
#38840=CARTESIAN_POINT('Ctrl Pts',(14.2259398250621,0.8277294809971,1.08333333333334));
#38841=CARTESIAN_POINT('Ctrl Pts',(14.2239464151202,0.861989623387911,0.949622058007612));
#38842=CARTESIAN_POINT('Ctrl Pts',(14.2222079250172,0.889808711690379,0.814376693553152));
#38843=CARTESIAN_POINT('Ctrl Pts',(14.2208398148552,0.911161325030034,0.678132403727965));
#38844=CARTESIAN_POINT('Ctrl Pts',(14.2194782068654,0.932412456504566,0.542535637670654));
#38845=CARTESIAN_POINT('Ctrl Pts',(14.2184834780892,0.947258512328438,0.40594941879874));
#38846=CARTESIAN_POINT('Ctrl Pts',(14.2179179597194,0.955671957676133,0.268901316711642));
#38847=CARTESIAN_POINT('Ctrl Pts',(14.2175487034788,0.961165532006069,0.179415511018676));
#38848=CARTESIAN_POINT('Ctrl Pts',(14.2173613909827,0.963916530720146,0.0897327832366183));
#38849=CARTESIAN_POINT('Ctrl Pts',(14.2173613909827,0.963916530720146,1.06581410364015E-14));
#38850=CARTESIAN_POINT('Ctrl Pts',(14.2173613909827,0.963916530720146,-0.13757393698032));
#38851=CARTESIAN_POINT('Ctrl Pts',(14.2178040883167,0.957451598945758,-0.274951212619625));
#38852=CARTESIAN_POINT('Ctrl Pts',(14.2186598102071,0.944570379379524,-0.411612406214599));
#38853=CARTESIAN_POINT('Ctrl Pts',(14.2195221530139,0.931589494866494,-0.549330978772693));
#38854=CARTESIAN_POINT('Ctrl Pts',(14.2208039138492,0.912092599491427,-0.686322345436757));
#38855=CARTESIAN_POINT('Ctrl Pts',(14.222421741201,0.886126297665472,-0.822054935347047));
#38856=CARTESIAN_POINT('Ctrl Pts',(14.2234666476786,0.869355437073955,-0.909720570537178));
#38857=CARTESIAN_POINT('Ctrl Pts',(14.2246506698206,0.849885807807131,-0.996861109122824));
#38858=CARTESIAN_POINT('Ctrl Pts',(14.2259398250621,0.827729480997101,-1.08333333333335));
#38859=CARTESIAN_POINT('',(15.1266902369927,0.687549796443762,-1.08333333333334));
#38860=CARTESIAN_POINT('Ctrl Pts',(14.2259398250621,0.827729480997104,-1.08333333333333));
#38861=CARTESIAN_POINT('Ctrl Pts',(14.4122867506183,0.85150138178118,-1.08333333333333));
#38862=CARTESIAN_POINT('Ctrl Pts',(14.6232724628281,0.840005933409977,-1.08333333333333));
#38863=CARTESIAN_POINT('Ctrl Pts',(14.9052713763609,0.775641521611009,-1.08333333333333));
#38864=CARTESIAN_POINT('Ctrl Pts',(15.0190662790554,0.73770573220136,-1.08333333333333));
#38865=CARTESIAN_POINT('Ctrl Pts',(15.1266902369927,0.687549796443768,-1.08333333333333));
#38866=CARTESIAN_POINT('Ctrl Pts',(15.1266902369927,0.687549796443768,-1.08333333333334));
#38867=CARTESIAN_POINT('Ctrl Pts',(15.1249773086751,0.725235701077452,-0.955915065626868));
#38868=CARTESIAN_POINT('Ctrl Pts',(15.1234319803901,0.756223536825589,-0.826701571451108));
#38869=CARTESIAN_POINT('Ctrl Pts',(15.122183667988,0.780412301388443,-0.696211209493001));
#38870=CARTESIAN_POINT('Ctrl Pts',(15.1209550316477,0.804219799510377,-0.567777653526322));
#38871=CARTESIAN_POINT('Ctrl Pts',(15.12001416535,0.821440959530357,-0.43810716485706));
#38872=CARTESIAN_POINT('Ctrl Pts',(15.1194343523859,0.831977831684773,-0.307693975182356));
#38873=CARTESIAN_POINT('Ctrl Pts',(15.1189800281283,0.840234212474528,-0.205506064179778));
#38874=CARTESIAN_POINT('Ctrl Pts',(15.1187464308798,0.844386527178536,-0.102862147741283));
#38875=CARTESIAN_POINT('Ctrl Pts',(15.1187464308798,0.844386527178536,-1.99840144432528E-15));
#38876=CARTESIAN_POINT('Ctrl Pts',(15.1187464308798,0.844386527178536,0.130666807305585));
#38877=CARTESIAN_POINT('Ctrl Pts',(15.1191251529677,0.837684329050871,0.261069786498764));
#38878=CARTESIAN_POINT('Ctrl Pts',(15.1198518432089,0.824355801783881,0.390710450871172));
#38879=CARTESIAN_POINT('Ctrl Pts',(15.1205872590302,0.810867235029882,0.521907748246314));
#38880=CARTESIAN_POINT('Ctrl Pts',(15.1216790167187,0.790592205023559,0.652324314224285));
#38881=CARTESIAN_POINT('Ctrl Pts',(15.1230415909943,0.763606761086929,0.781443489202972));
#38882=CARTESIAN_POINT('Ctrl Pts',(15.1241128691977,0.742390363262186,0.882959098491574));
#38883=CARTESIAN_POINT('Ctrl Pts',(15.1253504648421,0.717025942630064,0.983672743459537));
#38884=CARTESIAN_POINT('Ctrl Pts',(15.1266902369927,0.687549796443768,1.08333333333333));
#38885=CARTESIAN_POINT('',(13.3303603014235,-7.18268588222768,1.08333333333333));
#38886=CARTESIAN_POINT('',(12.4579905368411,-6.91816245718305,1.08333333333333));
#38887=CARTESIAN_POINT('Ctrl Pts',(13.3303603014235,-7.18268588222769,1.08333333333333));
#38888=CARTESIAN_POINT('Ctrl Pts',(13.2116326209361,-7.18117853359731,1.08333333333333));
#38889=CARTESIAN_POINT('Ctrl Pts',(13.0926472341269,-7.16598374096113,1.08333333333333));
#38890=CARTESIAN_POINT('Ctrl Pts',(12.8106483205942,-7.10161932916216,1.08333333333333));
#38891=CARTESIAN_POINT('Ctrl Pts',(12.6155690741987,-7.02043310055321,1.08333333333333));
#38892=CARTESIAN_POINT('Ctrl Pts',(12.4579905368414,-6.91816245718254,1.08333333333333));
#38893=CARTESIAN_POINT('',(13.3303603014235,-7.18268588222768,-1.08333333333334));
#38894=CARTESIAN_POINT('Ctrl Pts',(13.3303603014235,-7.18268588222769,1.08333333333333));
#38895=CARTESIAN_POINT('Ctrl Pts',(13.3126024326051,-7.21564274452345,0.956888632103319));
#38896=CARTESIAN_POINT('Ctrl Pts',(13.2978764135175,-7.24268913148574,0.828820583351199));
#38897=CARTESIAN_POINT('Ctrl Pts',(13.2863164700112,-7.26383348564869,0.699646919261793));
#38898=CARTESIAN_POINT('Ctrl Pts',(13.2748173090023,-7.28486666222208,0.57115245381317));
#38899=CARTESIAN_POINT('Ctrl Pts',(13.2664510227834,-7.30005980724128,0.441563969171537));
#38900=CARTESIAN_POINT('Ctrl Pts',(13.2613042752927,-7.30939745578421,0.311391073637702));
#38901=CARTESIAN_POINT('Ctrl Pts',(13.2561988309336,-7.31866016882124,0.182262827807302));
#38902=CARTESIAN_POINT('Ctrl Pts',(13.2542614634095,-7.32216103446727,0.0525595133519065));
#38903=CARTESIAN_POINT('Ctrl Pts',(13.2555318677529,-7.3198604598385,-0.0772214321948015));
#38904=CARTESIAN_POINT('Ctrl Pts',(13.2563983335702,-7.31829137729713,-0.16573715053459));
#38905=CARTESIAN_POINT('Ctrl Pts',(13.2587560588235,-7.31402308269219,-0.254288981130321));
#38906=CARTESIAN_POINT('Ctrl Pts',(13.2626054360147,-7.30703628683439,-0.342719102199534));
#38907=CARTESIAN_POINT('Ctrl Pts',(13.2684086950193,-7.29650310602066,-0.476034927301568));
#38908=CARTESIAN_POINT('Ctrl Pts',(13.2775701666805,-7.2798543418706,-0.608312350205377));
#38909=CARTESIAN_POINT('Ctrl Pts',(13.289943417625,-7.25719547792716,-0.739057191237071));
#38910=CARTESIAN_POINT('Ctrl Pts',(13.300929037023,-7.23707775329776,-0.8551392999939));
#38911=CARTESIAN_POINT('Ctrl Pts',(13.3144456587152,-7.21222189770271,-0.970013302477615));
#38912=CARTESIAN_POINT('Ctrl Pts',(13.3303603014235,-7.18268588222769,-1.08333333333334));
#38913=CARTESIAN_POINT('',(12.4579905368491,-6.91816245718746,-1.08333333333334));
#38914=CARTESIAN_POINT('Ctrl Pts',(13.3303603014235,-7.18268588222769,-1.08333333333333));
#38915=CARTESIAN_POINT('Ctrl Pts',(13.2116326209361,-7.18117853359731,-1.08333333333333));
#38916=CARTESIAN_POINT('Ctrl Pts',(13.0926472341269,-7.16598374096113,-1.08333333333333));
#38917=CARTESIAN_POINT('Ctrl Pts',(12.810648320597,-7.10161932916281,-1.08333333333333));
#38918=CARTESIAN_POINT('Ctrl Pts',(12.6155690742049,-7.020433100556,-1.08333333333333));
#38919=CARTESIAN_POINT('Ctrl Pts',(12.4579905368491,-6.91816245718749,-1.08333333333333));
#38920=CARTESIAN_POINT('Ctrl Pts',(12.4579905368414,-6.91816245718254,-1.08333333333318));
#38921=CARTESIAN_POINT('Ctrl Pts',(12.4412857888865,-6.94824379644432,-0.949270311030419));
#38922=CARTESIAN_POINT('Ctrl Pts',(12.4276027080704,-6.97263587945666,-0.813521288368017));
#38923=CARTESIAN_POINT('Ctrl Pts',(12.4170780656486,-6.99132836531005,-0.676607052101155));
#38924=CARTESIAN_POINT('Ctrl Pts',(12.4080806643215,-7.00730836636693,-0.559560573777918));
#38925=CARTESIAN_POINT('Ctrl Pts',(12.4013908554088,-7.019122574986,-0.441662516279092));
#38926=CARTESIAN_POINT('Ctrl Pts',(12.397067491958,-7.0267501449702,-0.323238258334718));
#38927=CARTESIAN_POINT('Ctrl Pts',(12.3920718206831,-7.03556384585387,-0.186398348762654));
#38928=CARTESIAN_POINT('Ctrl Pts',(12.3902516338787,-7.03876210460539,-0.0492519096262223));
#38929=CARTESIAN_POINT('Ctrl Pts',(12.3916053560035,-7.03637809537437,0.0876758270660355));
#38930=CARTESIAN_POINT('Ctrl Pts',(12.3929630026023,-7.03398717484161,0.225000520654302));
#38931=CARTESIAN_POINT('Ctrl Pts',(12.3975129673672,-7.02598155019911,0.362105241912753));
#38932=CARTESIAN_POINT('Ctrl Pts',(12.4052079364272,-7.01236879050172,0.498460177595601));
#38933=CARTESIAN_POINT('Ctrl Pts',(12.4129361026925,-6.99869730339771,0.635403368116608));
#38934=CARTESIAN_POINT('Ctrl Pts',(12.4238364813948,-6.9793701376568,0.771590289741124));
#38935=CARTESIAN_POINT('Ctrl Pts',(12.4378151222668,-6.95436948862457,0.906484242526394));
#38936=CARTESIAN_POINT('Ctrl Pts',(12.4439512822523,-6.94339503240884,0.96569821639967));
#38937=CARTESIAN_POINT('Ctrl Pts',(12.4506800022041,-6.93132701813272,1.0246630456538));
#38938=CARTESIAN_POINT('Ctrl Pts',(12.4579905368414,-6.91816245718254,1.08333333333318));
#38939=CARTESIAN_POINT('Origin',(13.892722748591,-3.17092330887735,-3.20017169526122E-15));
#38940=CARTESIAN_POINT('',(15.1423033840733,-0.0114224867026808,-1.08333333333334));
#38941=CARTESIAN_POINT('',(14.6487667980729,0.141522102769127,-1.08333333333334));
#38942=CARTESIAN_POINT('Origin',(13.892722748591,-3.17092330887735,-1.08333333333334));
#38943=CARTESIAN_POINT('',(13.1366786991091,-6.48336872052383,-1.08333333333334));
#38944=CARTESIAN_POINT('Origin',(13.892722748591,-3.17092330887735,-3.20017169526122E-15));
#38945=CARTESIAN_POINT('',(13.6476999686242,-6.55970790622078,-1.08333333333334));
#38946=CARTESIAN_POINT('Origin',(13.892722748591,-3.17092330887735,-1.08333333333334));
#38947=CARTESIAN_POINT('',(13.6476999686242,-6.55970790622078,1.08333333333333));
#38948=CARTESIAN_POINT('Ctrl Pts',(13.6476999686242,-6.55970790622078,-1.08333333333334));
#38949=CARTESIAN_POINT('Ctrl Pts',(13.5948858118209,-6.66958959248674,-0.727666221822799));
#38950=CARTESIAN_POINT('Ctrl Pts',(13.5683505740919,-6.72230205711255,-0.35278297384278));
#38951=CARTESIAN_POINT('Ctrl Pts',(13.5683505740919,-6.72230205711255,-3.93962482987281E-15));
#38952=CARTESIAN_POINT('Ctrl Pts',(13.5683505740919,-6.72230205711255,0.352782973842772));
#38953=CARTESIAN_POINT('Ctrl Pts',(13.5948858118209,-6.66958959248674,0.727666221822791));
#38954=CARTESIAN_POINT('Ctrl Pts',(13.6476999686242,-6.55970790622078,1.08333333333333));
#38955=CARTESIAN_POINT('',(12.7471768669564,-6.36961395396396,1.08333333333333));
#38956=CARTESIAN_POINT('Origin',(13.892722748591,-3.17092330887735,1.08333333333333));
#38957=CARTESIAN_POINT('',(12.7471768669564,-6.36961395396396,-1.08333333333334));
#38958=CARTESIAN_POINT('Ctrl Pts',(12.7471768669564,-6.36961395396397,1.08333333333334));
#38959=CARTESIAN_POINT('Ctrl Pts',(12.6958726976266,-6.47228631765585,0.725928647976583));
#38960=CARTESIAN_POINT('Ctrl Pts',(12.6703734952067,-6.52105325020152,0.352039859176988));
#38961=CARTESIAN_POINT('Ctrl Pts',(12.6703734952067,-6.52105325020152,-3.73360976135914E-15));
#38962=CARTESIAN_POINT('Ctrl Pts',(12.6703734952067,-6.52105325020152,-0.352039859176996));
#38963=CARTESIAN_POINT('Ctrl Pts',(12.6958726976266,-6.47228631765585,-0.72592864797659));
#38964=CARTESIAN_POINT('Ctrl Pts',(12.7471768669564,-6.36961395396397,-1.08333333333335));
#38965=CARTESIAN_POINT('Origin',(13.892722748591,-3.17092330887735,-1.08333333333334));
#38966=CARTESIAN_POINT('',(14.2484814298548,0.208031110850763,-1.08333333333334));
#38967=CARTESIAN_POINT('Origin',(13.892722748591,-3.17092330887735,-1.08333333333334));
#38968=CARTESIAN_POINT('',(14.2484814298548,0.208031110850763,1.08333333333333));
#38969=CARTESIAN_POINT('Ctrl Pts',(14.2484814298548,0.208031110850765,-1.08333333333334));
#38970=CARTESIAN_POINT('Ctrl Pts',(14.2468058395578,0.322795758952199,-0.725928647976584));
#38971=CARTESIAN_POINT('Ctrl Pts',(14.2449910310593,0.377796936249431,-0.352039859176992));
#38972=CARTESIAN_POINT('Ctrl Pts',(14.2449910310593,0.37779693624943,0.352039859176986));
#38973=CARTESIAN_POINT('Ctrl Pts',(14.2468058395578,0.322795758952199,0.725928647976576));
#38974=CARTESIAN_POINT('Ctrl Pts',(14.2484814298548,0.208031110850766,1.08333333333333));
#38975=CARTESIAN_POINT('',(15.1423033840733,-0.0114224867026808,1.08333333333333));
#38976=CARTESIAN_POINT('Origin',(13.892722748591,-3.17092330887735,1.08333333333333));
#38977=CARTESIAN_POINT('Ctrl Pts',(15.1423033840733,-0.0114224867026912,
1.08333333333333));
#38978=CARTESIAN_POINT('Ctrl Pts',(15.1423953499066,0.110492695607724,0.727666221822789));
#38979=CARTESIAN_POINT('Ctrl Pts',(15.1413590080604,0.169498193350193,0.352782973842772));
#38980=CARTESIAN_POINT('Ctrl Pts',(15.1413590080604,0.169498193350193,-0.352782973842778));
#38981=CARTESIAN_POINT('Ctrl Pts',(15.1423953499066,0.110492695607724,-0.727666221822797));
#38982=CARTESIAN_POINT('Ctrl Pts',(15.1423033840733,-0.0114224867026924,
-1.08333333333334));
#38983=CARTESIAN_POINT('',(13.0227870731057,-2.97236616780865,3.45272288248773));
#38984=CARTESIAN_POINT('Origin',(13.0227870731057,-2.97236616780865,-2.9997830762867E-15));
#38985=CARTESIAN_POINT('',(14.7626584240763,-3.36948044994605,3.45272288248773));
#38986=CARTESIAN_POINT('Origin',(14.7626584240763,-3.36948044994605,-3.40056031423575E-15));
#38987=CARTESIAN_POINT('Origin',(11.1410986251693,8.88472967648709,-9.85584169237555E-16));
#38988=CARTESIAN_POINT('',(11.8387328710639,9.44107442276104,-3.96060240207311));
#38989=CARTESIAN_POINT('Origin',(11.8387328710639,9.44107442276104,-1.0472995612114E-15));
#38990=CARTESIAN_POINT('',(10.4434643792748,8.32838493021314,-3.96060240207311));
#38991=CARTESIAN_POINT('Origin',(11.1410986251693,8.88472967648709,-2.5198520116158));
#38992=CARTESIAN_POINT('Origin',(10.4434643792748,8.32838493021314,-9.23868777263706E-16));
#38993=CARTESIAN_POINT('',(8.89378902201275,12.2552029391784,1.08333333331655));
#38994=CARTESIAN_POINT('',(8.89378902201677,12.2552029391754,-1.08333333333333));
#38995=CARTESIAN_POINT('Ctrl Pts',(8.89378902201274,12.2552029391784,1.08333333331655));
#38996=CARTESIAN_POINT('Ctrl Pts',(8.86335293025879,12.2772908784853,0.956315399884826));
#38997=CARTESIAN_POINT('Ctrl Pts',(8.83824313040494,12.2953456493747,0.827586922367285));
#38998=CARTESIAN_POINT('Ctrl Pts',(8.81859777764014,12.3094197866805,0.69766772380084));
#38999=CARTESIAN_POINT('Ctrl Pts',(8.7991879276401,12.3233252073292,0.569305958731489));
#39000=CARTESIAN_POINT('Ctrl Pts',(8.78511225071473,12.3333449381983,0.439781849534452));
#39001=CARTESIAN_POINT('Ctrl Pts',(8.77647376760361,12.3394890678296,0.309596747993595));
#39002=CARTESIAN_POINT('Ctrl Pts',(8.76964787761092,12.344343988818,0.206728088024587));
#39003=CARTESIAN_POINT('Ctrl Pts',(8.76621624622163,12.3467783236357,0.103446722778746));
#39004=CARTESIAN_POINT('Ctrl Pts',(8.76621624622163,12.3467783236357,7.54951656745106E-15));
#39005=CARTESIAN_POINT('Ctrl Pts',(8.76621624622163,12.3467783236357,-0.130951008152141));
#39006=CARTESIAN_POINT('Ctrl Pts',(8.77171477448527,12.3428797767713,-0.261548325668487));
#39007=CARTESIAN_POINT('Ctrl Pts',(8.78261416841303,12.3351194002049,-0.391301356121213));
#39008=CARTESIAN_POINT('Ctrl Pts',(8.79368558213778,12.3272365454154,-0.523102215114213));
#39009=CARTESIAN_POINT('Ctrl Pts',(8.81032969837903,12.3153689336875,-0.654031926803563));
#39010=CARTESIAN_POINT('Ctrl Pts',(8.83241243050519,12.2995110840219,-0.783576297698762));
#39011=CARTESIAN_POINT('Ctrl Pts',(8.84960195907419,12.2871670969504,-0.88441557119687));
#39012=CARTESIAN_POINT('Ctrl Pts',(8.87008627043973,12.2724043900869,-0.984415425401903));
#39013=CARTESIAN_POINT('Ctrl Pts',(8.89378902201675,12.2552029391755,-1.08333333333333));
#39014=CARTESIAN_POINT('',(8.22258343557175,11.6383685130288,1.08333333333333));
#39015=CARTESIAN_POINT('Ctrl Pts',(8.89378902201473,12.2552029391744,1.08333333333333));
#39016=CARTESIAN_POINT('Ctrl Pts',(8.7875190745609,12.202353722575,1.08333333333333));
#39017=CARTESIAN_POINT('Ctrl Pts',(8.68681488082435,12.1369760343753,1.08333333333333));
#39018=CARTESIAN_POINT('Ctrl Pts',(8.46069343470619,11.9566501984405,1.08333333333333));
#39019=CARTESIAN_POINT('Ctrl Pts',(8.31988542322913,11.7983921800676,1.08333333333333));
#39020=CARTESIAN_POINT('Ctrl Pts',(8.22258343557172,11.6383685130288,1.08333333333333));
#39021=CARTESIAN_POINT('',(8.22258343557123,11.6383685130292,-1.08333333333333));
#39022=CARTESIAN_POINT('Ctrl Pts',(8.2225834355717,11.6383685130289,-1.08333333333318));
#39023=CARTESIAN_POINT('Ctrl Pts',(8.19448780675769,11.6582182584498,-0.949301954017324));
#39024=CARTESIAN_POINT('Ctrl Pts',(8.17159767874311,11.6742430454627,-0.81366496302888));
#39025=CARTESIAN_POINT('Ctrl Pts',(8.15402161030241,11.6865063889394,-0.67695567866062));
#39026=CARTESIAN_POINT('Ctrl Pts',(8.13658119548769,11.6986750828637,-0.541301528447691));
#39027=CARTESIAN_POINT('Ctrl Pts',(8.12437307855494,11.7071402381473,-0.40459157308691));
#39028=CARTESIAN_POINT('Ctrl Pts',(8.1174733585697,11.7119223986889,-0.26734687734235));
#39029=CARTESIAN_POINT('Ctrl Pts',(8.11300215046573,11.7150213700985,-0.178408544025479));
#39030=CARTESIAN_POINT('Ctrl Pts',(8.11075954642938,11.7165728598428,-0.0892456520429063));
#39031=CARTESIAN_POINT('Ctrl Pts',(8.11075954642938,11.7165728598428,1.33226762955019E-15));
#39032=CARTESIAN_POINT('Ctrl Pts',(8.11075954642938,11.7165728598428,0.137335411050026));
#39033=CARTESIAN_POINT('Ctrl Pts',(8.11607262981309,11.7129002012938,0.274553571737022));
#39034=CARTESIAN_POINT('Ctrl Pts',(8.12665801674411,11.7055512249056,0.411127959090392));
#39035=CARTESIAN_POINT('Ctrl Pts',(8.13729388250879,11.698167203246,0.548353632582512));
#39036=CARTESIAN_POINT('Ctrl Pts',(8.15325248641432,11.6870716767896,0.684929378140945));
#39037=CARTESIAN_POINT('Ctrl Pts',(8.17446212457132,11.6722178258439,0.820321104282498));
#39038=CARTESIAN_POINT('Ctrl Pts',(8.18828255682692,11.6625388940673,0.908543834215877));
#39039=CARTESIAN_POINT('Ctrl Pts',(8.20433194575505,11.6512633098961,0.9962638332735));
#39040=CARTESIAN_POINT('Ctrl Pts',(8.22258343557176,11.6383685130288,1.08333333333334));
#39041=CARTESIAN_POINT('Ctrl Pts',(8.89378902201675,12.2552029391755,-1.08333333333333));
#39042=CARTESIAN_POINT('Ctrl Pts',(8.78751907456219,12.2023537225759,-1.08333333333333));
#39043=CARTESIAN_POINT('Ctrl Pts',(8.68681488082489,12.1369760343758,-1.08333333333333));
#39044=CARTESIAN_POINT('Ctrl Pts',(8.46069343470621,11.9566501984405,-1.08333333333333));
#39045=CARTESIAN_POINT('Ctrl Pts',(8.31988542322917,11.7983921800676,-1.08333333333333));
#39046=CARTESIAN_POINT('Ctrl Pts',(8.22258343557176,11.6383685130289,-1.08333333333333));
#39047=CARTESIAN_POINT('',(13.9269936544443,5.94376395877129,1.08333333333333));
#39048=CARTESIAN_POINT('',(13.1762672612271,5.42664547033562,1.08333333333333));
#39049=CARTESIAN_POINT('Ctrl Pts',(13.9269936544443,5.94376395877129,1.08333333333333));
#39050=CARTESIAN_POINT('Ctrl Pts',(13.8517896638478,5.85187873682469,1.08333333333333));
#39051=CARTESIAN_POINT('Ctrl Pts',(13.7657237213495,5.76832601371371,1.08333333333333));
#39052=CARTESIAN_POINT('Ctrl Pts',(13.5395781511316,5.5879809394513,1.08333333333333));
#39053=CARTESIAN_POINT('Ctrl Pts',(13.3544742809805,5.48608062863226,1.08333333333333));
#39054=CARTESIAN_POINT('Ctrl Pts',(13.1762672612269,5.42664547033621,1.08333333333333));
#39055=CARTESIAN_POINT('',(13.9269936544443,5.94376395877129,-1.08333333333333));
#39056=CARTESIAN_POINT('Ctrl Pts',(13.9269936544443,5.9437639587713,1.08333333333333));
#39057=CARTESIAN_POINT('Ctrl Pts',(13.9416885168395,5.90933203032488,0.95688863210334));
#39058=CARTESIAN_POINT('Ctrl Pts',(13.9536527109305,5.88095561854266,0.828820583351241));
#39059=CARTESIAN_POINT('Ctrl Pts',(13.9629765258053,5.85873440158633,0.699646919261855));
#39060=CARTESIAN_POINT('Ctrl Pts',(13.9722513158077,5.83663002439342,0.571152453813261));
#39061=CARTESIAN_POINT('Ctrl Pts',(13.9789135007645,5.82061622745854,0.441563969171658));
#39062=CARTESIAN_POINT('Ctrl Pts',(13.9830050237944,5.81077040959811,0.31139107363785));
#39063=CARTESIAN_POINT('Ctrl Pts',(13.987063711968,5.80100360535004,0.182262827807452));
#39064=CARTESIAN_POINT('Ctrl Pts',(13.9885928700522,5.79730615639857,0.0525595133520559));
#39065=CARTESIAN_POINT('Ctrl Pts',(13.9875862925321,5.79973378332923,-0.077221432194654));
#39066=CARTESIAN_POINT('Ctrl Pts',(13.9868997670033,5.80138952054645,-0.165737150534494));
#39067=CARTESIAN_POINT('Ctrl Pts',(13.9850326975557,5.80589410253397,-0.254288981130278));
#39068=CARTESIAN_POINT('Ctrl Pts',(13.9819702480148,5.81325986277498,-0.342719102199545));
#39069=CARTESIAN_POINT('Ctrl Pts',(13.977353348451,5.82436436418423,-0.476034927301432));
#39070=CARTESIAN_POINT('Ctrl Pts',(13.9700489046451,5.84190742581571,-0.608312350205104));
#39071=CARTESIAN_POINT('Ctrl Pts',(13.9600480872369,5.86570879353505,-0.739057191236667));
#39072=CARTESIAN_POINT('Ctrl Pts',(13.9511688384277,5.88684089277784,-0.855139299993628));
#39073=CARTESIAN_POINT('Ctrl Pts',(13.9401632237805,5.91290598563348,-0.970013302477476));
#39074=CARTESIAN_POINT('Ctrl Pts',(13.9269936544443,5.9437639587713,-1.08333333333333));
#39075=CARTESIAN_POINT('',(13.1762672612355,5.42664547033908,-1.08333333333333));
#39076=CARTESIAN_POINT('Ctrl Pts',(13.9269936544443,5.94376395877129,-1.08333333333333));
#39077=CARTESIAN_POINT('Ctrl Pts',(13.8517896638478,5.85187873682469,-1.08333333333333));
#39078=CARTESIAN_POINT('Ctrl Pts',(13.7657237213495,5.76832601371371,-1.08333333333333));
#39079=CARTESIAN_POINT('Ctrl Pts',(13.5395781511339,5.5879809394531,-1.08333333333333));
#39080=CARTESIAN_POINT('Ctrl Pts',(13.3544742809865,5.48608062863536,-1.08333333333333));
#39081=CARTESIAN_POINT('Ctrl Pts',(13.1762672612355,5.42664547033908,-1.08333333333333));
#39082=CARTESIAN_POINT('Ctrl Pts',(13.1762672612269,5.42664547033617,-1.08333333333318));
#39083=CARTESIAN_POINT('Ctrl Pts',(13.1893705593041,5.39482976422236,-0.949270311030452));
#39084=CARTESIAN_POINT('Ctrl Pts',(13.1999097963792,5.36892368585892,-0.813521288368082));
#39085=CARTESIAN_POINT('Ctrl Pts',(13.2079621630868,5.34904061477083,-0.676607052101254));
#39086=CARTESIAN_POINT('Ctrl Pts',(13.2148460430323,5.33204279546023,-0.559560573777983));
#39087=CARTESIAN_POINT('Ctrl Pts',(13.2199117356377,5.31944645364959,-0.441662516279123));
#39088=CARTESIAN_POINT('Ctrl Pts',(13.2231796369647,5.31131059989547,-0.323238258334714));
#39089=CARTESIAN_POINT('Ctrl Pts',(13.2269557156993,5.30190957419912,-0.186398348762647));
#39090=CARTESIAN_POINT('Ctrl Pts',(13.2283213471703,5.2984924131362,-0.0492519096262126));
#39091=CARTESIAN_POINT('Ctrl Pts',(13.2273014856384,5.30103720115497,0.087675827066048));
#39092=CARTESIAN_POINT('Ctrl Pts',(13.2262786675026,5.30358936657715,0.225000520654307));
#39093=CARTESIAN_POINT('Ctrl Pts',(13.22285647475,5.31213809759657,0.362105241912749));
#39094=CARTESIAN_POINT('Ctrl Pts',(13.2170113253899,5.32664168351083,0.498460177595588));
#39095=CARTESIAN_POINT('Ctrl Pts',(13.2111409592133,5.34120783998435,0.635403368116607));
#39096=CARTESIAN_POINT('Ctrl Pts',(13.2028266475275,5.36178038996296,0.771590289741134));
#39097=CARTESIAN_POINT('Ctrl Pts',(13.1919958930594,5.38829698119018,0.906484242526414));
#39098=CARTESIAN_POINT('Ctrl Pts',(13.1872415508606,5.3999368857798,0.965698216399684));
#39099=CARTESIAN_POINT('Ctrl Pts',(13.1820016856381,5.41272189470467,1.02466304565381));
#39100=CARTESIAN_POINT('Ctrl Pts',(13.1762672612269,5.42664547033617,1.08333333333318));
#39101=CARTESIAN_POINT('Origin',(11.1410986251693,8.88472967648709,-9.85584169237555E-16));
#39102=CARTESIAN_POINT('',(8.72113759169208,11.2696166353064,-1.08333333333333));
#39103=CARTESIAN_POINT('',(9.02271027299523,11.54110464988,-1.08333333333333));
#39104=CARTESIAN_POINT('Origin',(11.1410986251693,8.88472967648709,-1.08333333333333));
#39105=CARTESIAN_POINT('',(8.72113759169208,11.2696166353064,1.08333333333333));
#39106=CARTESIAN_POINT('Ctrl Pts',(8.72113759169207,11.2696166353064,1.08333333333334));
#39107=CARTESIAN_POINT('Ctrl Pts',(8.63036626326973,11.3398611937657,0.725928647976583));
#39108=CARTESIAN_POINT('Ctrl Pts',(8.5862330966948,11.3727349924819,0.35203985917699));
#39109=CARTESIAN_POINT('Ctrl Pts',(8.5862330966948,11.3727349924819,-0.352039859176991));
#39110=CARTESIAN_POINT('Ctrl Pts',(8.63036626326973,11.3398611937657,-0.725928647976582));
#39111=CARTESIAN_POINT('Ctrl Pts',(8.72113759169207,11.2696166353064,-1.08333333333334));
#39112=CARTESIAN_POINT('',(9.4500021963329,11.8316076987797,1.08333333333333));
#39113=CARTESIAN_POINT('Origin',(11.1410986251693,8.88472967648709,1.08333333333333));
#39114=CARTESIAN_POINT('',(9.4500021963329,11.8316076987797,-1.08333333333333));
#39115=CARTESIAN_POINT('Ctrl Pts',(9.4500021963329,11.8316076987798,-1.08333333333334));
#39116=CARTESIAN_POINT('Ctrl Pts',(9.35474240837097,11.9076924734258,-0.7276662218228));
#39117=CARTESIAN_POINT('Ctrl Pts',(9.30796390402485,11.9436715548399,-0.352782973842779));
#39118=CARTESIAN_POINT('Ctrl Pts',(9.30796390402485,11.9436715548399,0.352782973842777));
#39119=CARTESIAN_POINT('Ctrl Pts',(9.35474240837097,11.9076924734258,0.727666221822799));
#39120=CARTESIAN_POINT('Ctrl Pts',(9.4500021963329,11.8316076987798,1.08333333333334));
#39121=CARTESIAN_POINT('Origin',(11.1410986251693,8.88472967648709,-1.08333333333333));
#39122=CARTESIAN_POINT('',(13.2594869773434,6.22835470309422,-1.08333333333333));
#39123=CARTESIAN_POINT('Origin',(11.1410986251693,8.88472967648709,-9.85584169237555E-16));
#39124=CARTESIAN_POINT('',(13.6377879061428,6.58029051604763,-1.08333333333333));
#39125=CARTESIAN_POINT('Origin',(11.1410986251693,8.88472967648709,-1.08333333333333));
#39126=CARTESIAN_POINT('',(13.6377879061428,6.58029051604763,1.08333333333333));
#39127=CARTESIAN_POINT('Ctrl Pts',(13.6377879061428,6.58029051604764,-1.08333333333332));
#39128=CARTESIAN_POINT('Ctrl Pts',(13.6907677796515,6.47048863474093,-0.727666221822788));
#39129=CARTESIAN_POINT('Ctrl Pts',(13.7154355939006,6.41687686636464,-0.352782973842773));
#39130=CARTESIAN_POINT('Ctrl Pts',(13.7154355939006,6.41687686636464,-9.86054494281319E-16));
#39131=CARTESIAN_POINT('Ctrl Pts',(13.7154355939006,6.41687686636464,0.352782973842772));
#39132=CARTESIAN_POINT('Ctrl Pts',(13.6907677796515,6.47048863474094,0.727666221822788));
#39133=CARTESIAN_POINT('Ctrl Pts',(13.6377879061428,6.58029051604764,1.08333333333332));
#39134=CARTESIAN_POINT('',(12.9276994994135,5.9947548451011,1.08333333333333));
#39135=CARTESIAN_POINT('Origin',(11.1410986251693,8.88472967648709,1.08333333333333));
#39136=CARTESIAN_POINT('',(12.9276994994135,5.9947548451011,-1.08333333333333));
#39137=CARTESIAN_POINT('Ctrl Pts',(12.9276994994135,5.9947548451011,1.08333333333333));
#39138=CARTESIAN_POINT('Ctrl Pts',(12.9759843593573,5.89062845864264,0.72592864797658));
#39139=CARTESIAN_POINT('Ctrl Pts',(12.9982133898606,5.84028669430273,0.352039859176989));
#39140=CARTESIAN_POINT('Ctrl Pts',(12.9982133898606,5.84028669430273,-9.85141416048961E-16));
#39141=CARTESIAN_POINT('Ctrl Pts',(12.9982133898606,5.84028669430273,-0.35203985917699));
#39142=CARTESIAN_POINT('Ctrl Pts',(12.9759843593573,5.89062845864264,-0.72592864797658));
#39143=CARTESIAN_POINT('Ctrl Pts',(12.9276994994135,5.9947548451011,-1.08333333333333));
#39144=CARTESIAN_POINT('Origin',(11.1410986251693,8.88472967648709,-1.08333333333333));
#39145=CARTESIAN_POINT('',(10.4434643792748,8.32838493021314,3.45272288248773));
#39146=CARTESIAN_POINT('Origin',(10.4434643792748,8.32838493021314,-9.23868777263706E-16));
#39147=CARTESIAN_POINT('',(11.8387328710639,9.44107442276105,3.45272288248773));
#39148=CARTESIAN_POINT('Origin',(11.8387328710639,9.44107442276104,-1.0472995612114E-15));
#39149=CARTESIAN_POINT('Origin',(0.,14.25,0.));
#39150=CARTESIAN_POINT('',(-3.35834339016074,14.7651959662676,-1.08333333333333));
#39151=CARTESIAN_POINT('',(-3.39763111739558,14.25,-1.08333333333333));
#39152=CARTESIAN_POINT('Origin',(1.55588456152529E-16,14.25,-1.08333333333333));
#39153=CARTESIAN_POINT('',(3.39763111739558,14.25,-1.08333333333333));
#39154=CARTESIAN_POINT('Origin',(0.,14.25,0.));
#39155=CARTESIAN_POINT('',(3.35834339016074,14.7651959662676,-1.08333333333333));
#39156=CARTESIAN_POINT('Origin',(0.,14.25,-1.08333333333333));
#39157=CARTESIAN_POINT('',(3.35834339016074,14.7651959662676,1.08333333333333));
#39158=CARTESIAN_POINT('Ctrl Pts',(3.35834339016074,14.7651959662676,-1.08333333333333));
#39159=CARTESIAN_POINT('Ctrl Pts',(3.47722236863702,14.7381569460943,-0.727666221822793));
#39160=CARTESIAN_POINT('Ctrl Pts',(3.53451786760282,14.7240166290356,-0.352782973842775));
#39161=CARTESIAN_POINT('Ctrl Pts',(3.53451786760282,14.7240166290356,0.));
#39162=CARTESIAN_POINT('Ctrl Pts',(3.53451786760282,14.7240166290356,0.352782973842776));
#39163=CARTESIAN_POINT('Ctrl Pts',(3.47722236863702,14.7381569460943,0.727666221822795));
#39164=CARTESIAN_POINT('Ctrl Pts',(3.35834339016074,14.7651959662676,1.08333333333333));
#39165=CARTESIAN_POINT('',(3.37340073180097,13.8449509750914,1.08333333333333));
#39166=CARTESIAN_POINT('Origin',(0.,14.25,1.08333333333333));
#39167=CARTESIAN_POINT('',(3.37340073180097,13.8449509750914,-1.08333333333333));
#39168=CARTESIAN_POINT('Ctrl Pts',(3.37340073180098,13.8449509750914,1.08333333333333));
#39169=CARTESIAN_POINT('Ctrl Pts',(3.48491513664897,13.8177798586608,0.725928647976577));
#39170=CARTESIAN_POINT('Ctrl Pts',(3.53813348671686,13.8037716378594,0.352039859176988));
#39171=CARTESIAN_POINT('Ctrl Pts',(3.53813348671686,13.8037716378594,0.));
#39172=CARTESIAN_POINT('Ctrl Pts',(3.53813348671686,13.8037716378594,-0.352039859176988));
#39173=CARTESIAN_POINT('Ctrl Pts',(3.48491513664897,13.8177798586608,-0.725928647976578));
#39174=CARTESIAN_POINT('Ctrl Pts',(3.37340073180098,13.8449509750914,-1.08333333333333));
#39175=CARTESIAN_POINT('Origin',(0.,14.25,-1.08333333333333));
#39176=CARTESIAN_POINT('',(-3.37340073180097,13.8449509750914,-1.08333333333333));
#39177=CARTESIAN_POINT('Origin',(1.55588456152529E-16,14.25,-1.08333333333333));
#39178=CARTESIAN_POINT('',(-3.37340073180097,13.8449509750914,1.08333333333333));
#39179=CARTESIAN_POINT('Ctrl Pts',(-3.37340073180098,13.8449509750914,-1.08333333333333));
#39180=CARTESIAN_POINT('Ctrl Pts',(-3.48491513664897,13.8177798586608,-0.725928647976578));
#39181=CARTESIAN_POINT('Ctrl Pts',(-3.53813348671686,13.8037716378594,-0.352039859176988));
#39182=CARTESIAN_POINT('Ctrl Pts',(-3.53813348671686,13.8037716378594,0.352039859176988));
#39183=CARTESIAN_POINT('Ctrl Pts',(-3.48491513664897,13.8177798586608,0.725928647976578));
#39184=CARTESIAN_POINT('Ctrl Pts',(-3.37340073180098,13.8449509750914,1.08333333333333));
#39185=CARTESIAN_POINT('',(-3.35834339016074,14.7651959662676,1.08333333333333));
#39186=CARTESIAN_POINT('Origin',(-1.5558845615253E-16,14.25,1.08333333333333));
#39187=CARTESIAN_POINT('Ctrl Pts',(-3.35834339016074,14.7651959662676,1.08333333333333));
#39188=CARTESIAN_POINT('Ctrl Pts',(-3.47722236863702,14.7381569460943,0.727666221822794));
#39189=CARTESIAN_POINT('Ctrl Pts',(-3.53451786760282,14.7240166290356,0.352782973842775));
#39190=CARTESIAN_POINT('Ctrl Pts',(-3.53451786760282,14.7240166290356,-0.352782973842776));
#39191=CARTESIAN_POINT('Ctrl Pts',(-3.47722236863702,14.7381569460943,-0.727666221822794));
#39192=CARTESIAN_POINT('Ctrl Pts',(-3.35834339016074,14.7651959662676,-1.08333333333333));
#39193=CARTESIAN_POINT('',(0.,13.3576923076923,3.45272288248773));
#39194=CARTESIAN_POINT('Origin',(0.,13.3576923076923,0.));
#39195=CARTESIAN_POINT('',(0.,15.1423076923077,3.45272288248773));
#39196=CARTESIAN_POINT('Origin',(0.,15.1423076923077,0.));
#39197=CARTESIAN_POINT('Origin',(0.,14.25,0.));
#39198=CARTESIAN_POINT('',(-4.85033905439415E-16,15.1423076923077,-3.96060240207311));
#39199=CARTESIAN_POINT('Origin',(0.,15.1423076923077,0.));
#39200=CARTESIAN_POINT('',(-4.85033905439415E-16,13.3576923076923,-3.96060240207311));
#39201=CARTESIAN_POINT('Origin',(-3.08592870035031E-16,14.25,-2.5198520116158));
#39202=CARTESIAN_POINT('Origin',(0.,13.3576923076923,0.));
#39203=CARTESIAN_POINT('',(-3.97254599103887,13.6850786752975,1.08333333333333));
#39204=CARTESIAN_POINT('',(-4.03631672677061,14.5944383081266,1.08333333333333));
#39205=CARTESIAN_POINT('Ctrl Pts',(-3.97254599103889,13.6850786752975,1.08333333333333));
#39206=CARTESIAN_POINT('Ctrl Pts',(-4.03699073486477,13.8609255570095,1.08333333333333));
#39207=CARTESIAN_POINT('Ctrl Pts',(-4.07292947680577,14.0696859538838,1.08333333333333));
#39208=CARTESIAN_POINT('Ctrl Pts',(-4.07292947680577,14.358906139038,1.08333333333333));
#39209=CARTESIAN_POINT('Ctrl Pts',(-4.06125577389194,14.4784021699804,1.08333333333333));
#39210=CARTESIAN_POINT('Ctrl Pts',(-4.03631672677123,14.5944383081267,1.08333333333333));
#39211=CARTESIAN_POINT('',(-3.97254599103887,13.6850786752975,-1.08333333333333));
#39212=CARTESIAN_POINT('Ctrl Pts',(-3.97254599103885,13.6850786752975,1.08333333333333));
#39213=CARTESIAN_POINT('Ctrl Pts',(-4.0055902844374,13.6754864779574,0.949270311030653));
#39214=CARTESIAN_POINT('Ctrl Pts',(-4.03241557892495,13.6675742096383,0.813521288368336));
#39215=CARTESIAN_POINT('Ctrl Pts',(-4.05298135839275,13.6614729113855,0.67660705210156));
#39216=CARTESIAN_POINT('Ctrl Pts',(-4.07056281760631,13.6562569784544,0.559560573778188));
#39217=CARTESIAN_POINT('Ctrl Pts',(-4.08356944187665,13.6523638057542,0.441662516279225));
#39218=CARTESIAN_POINT('Ctrl Pts',(-4.09196781162929,13.6498461320482,0.32323825833471));
#39219=CARTESIAN_POINT('Ctrl Pts',(-4.10167217606822,13.6469369456345,0.186398348762652));
#39220=CARTESIAN_POINT('Ctrl Pts',(-4.10519527746315,13.6458740742379,0.0492519096262281));
#39221=CARTESIAN_POINT('Ctrl Pts',(-4.1025698088094,13.6466633637621,-0.0876758270660229));
#39222=CARTESIAN_POINT('Ctrl Pts',(-4.09993672885708,13.6474549414561,-0.225000520654293));
#39223=CARTESIAN_POINT('Ctrl Pts',(-4.0911193595297,13.6501094100325,-0.362105241912746));
#39224=CARTESIAN_POINT('Ctrl Pts',(-4.07613560843688,13.6545823261509,-0.498460177595596));
#39225=CARTESIAN_POINT('Ctrl Pts',(-4.06108721528303,13.659074539074,-0.635403368116582));
#39226=CARTESIAN_POINT('Ctrl Pts',(-4.03981905948952,13.6654009235528,-0.771590289741077));
#39227=CARTESIAN_POINT('Ctrl Pts',(-4.01233468870309,13.673465922941,-0.906484242526326));
#39228=CARTESIAN_POINT('Ctrl Pts',(-4.00026996096645,13.6770061903378,-0.965698216399675));
#39229=CARTESIAN_POINT('Ctrl Pts',(-3.98700723595603,13.6808808214243,-1.02466304565388));
#39230=CARTESIAN_POINT('Ctrl Pts',(-3.97254599103885,13.6850786752975,-1.08333333333333));
#39231=CARTESIAN_POINT('',(-4.03631672677098,14.5944383081279,-1.08333333333333));
#39232=CARTESIAN_POINT('Ctrl Pts',(-3.97254599103889,13.6850786752975,-1.08333333333333));
#39233=CARTESIAN_POINT('Ctrl Pts',(-4.03718797255354,13.8614637488071,-1.08333333333333));
#39234=CARTESIAN_POINT('Ctrl Pts',(-4.07292947680577,14.0697175866198,-1.08333333333333));
#39235=CARTESIAN_POINT('Ctrl Pts',(-4.07292947680577,14.3589686276554,-1.08333333333333));
#39236=CARTESIAN_POINT('Ctrl Pts',(-4.06126656486658,14.4783519618466,-1.08333333333333));
#39237=CARTESIAN_POINT('Ctrl Pts',(-4.03631672677098,14.5944383081279,-1.08333333333333));
#39238=CARTESIAN_POINT('Ctrl Pts',(-4.03631672677125,14.5944383081264,-1.08333333333353));
#39239=CARTESIAN_POINT('Ctrl Pts',(-4.07239878927587,14.5844592579328,-0.956888632103535));
#39240=CARTESIAN_POINT('Ctrl Pts',(-4.10204391436992,14.576120838176,-0.828820583351431));
#39241=CARTESIAN_POINT('Ctrl Pts',(-4.12523046485396,14.5695557880246,-0.699646919262042));
#39242=CARTESIAN_POINT('Ctrl Pts',(-4.14829509982461,14.5630252570856,-0.571152453813459));
#39243=CARTESIAN_POINT('Ctrl Pts',(-4.16496899480084,14.5582495239489,-0.441563969171867));
#39244=CARTESIAN_POINT('Ctrl Pts',(-4.17521778805797,14.555309638438,-0.311391073638072));
#39245=CARTESIAN_POINT('Ctrl Pts',(-4.18538433378736,14.5523933457842,-0.182262827807668));
#39246=CARTESIAN_POINT('Ctrl Pts',(-4.18922853025337,14.5512835680019,-0.0525595133522669));
#39247=CARTESIAN_POINT('Ctrl Pts',(-4.18670294427272,14.5520101946411,0.0772214321944475));
#39248=CARTESIAN_POINT('Ctrl Pts',(-4.18498039512374,14.5525057826387,0.165737150534356));
#39249=CARTESIAN_POINT('Ctrl Pts',(-4.1802944723506,14.5538546098955,0.254288981130209));
#39250=CARTESIAN_POINT('Ctrl Pts',(-4.17262628304436,14.5560527668241,0.342719102199544));
#39251=CARTESIAN_POINT('Ctrl Pts',(-4.16106584445129,14.5593666727772,0.476034927301542));
#39252=CARTESIAN_POINT('Ctrl Pts',(-4.14279588034764,14.5645937486684,0.608312350205319));
#39253=CARTESIAN_POINT('Ctrl Pts',(-4.11795181407459,14.5716147048116,0.739057191236983));
#39254=CARTESIAN_POINT('Ctrl Pts',(-4.09589395251526,14.5778482769217,0.855139299993905));
#39255=CARTESIAN_POINT('Ctrl Pts',(-4.06865355383155,14.5854950604866,0.970013302477714));
#39256=CARTESIAN_POINT('Ctrl Pts',(-4.03631672677125,14.5944383081264,1.08333333333353));
#39257=CARTESIAN_POINT('',(4.0363167267713,14.5944383081264,1.08333333333333));
#39258=CARTESIAN_POINT('',(3.97254599103947,13.6850786752973,1.08333333333333));
#39259=CARTESIAN_POINT('Ctrl Pts',(4.0363167267713,14.5944383081264,1.08333333333333));
#39260=CARTESIAN_POINT('Ctrl Pts',(4.06125577389196,14.4784021699801,1.08333333333333));
#39261=CARTESIAN_POINT('Ctrl Pts',(4.07292947680577,14.3589061390379,1.08333333333333));
#39262=CARTESIAN_POINT('Ctrl Pts',(4.07292947680577,14.0696859538838,1.08333333333333));
#39263=CARTESIAN_POINT('Ctrl Pts',(4.03699073486477,13.8609255570095,1.08333333333333));
#39264=CARTESIAN_POINT('Ctrl Pts',(3.97254599103889,13.6850786752975,1.08333333333333));
#39265=CARTESIAN_POINT('',(4.0363167267713,14.5944383081264,-1.08333333333333));
#39266=CARTESIAN_POINT('Ctrl Pts',(4.0363167267713,14.5944383081264,1.08333333333333));
#39267=CARTESIAN_POINT('Ctrl Pts',(4.07267660468553,14.5843824238018,0.955915065626592));
#39268=CARTESIAN_POINT('Ctrl Pts',(4.10254364280131,14.5759803979714,0.826701571450557));
#39269=CARTESIAN_POINT('Ctrl Pts',(4.12584816889326,14.5693808768856,0.696211209492171));
#39270=CARTESIAN_POINT('Ctrl Pts',(4.14878536602558,14.5628853783063,0.567777653525462));
#39271=CARTESIAN_POINT('Ctrl Pts',(4.16536539316191,14.5581360328796,0.438107164856169));
#39272=CARTESIAN_POINT('Ctrl Pts',(4.17550906341001,14.5552260824043,0.307693975181436));
#39273=CARTESIAN_POINT('Ctrl Pts',(4.18345734283739,14.55294593144,0.205506064179161));
#39274=CARTESIAN_POINT('Ctrl Pts',(4.18745357006455,14.5517942140162,0.102862147740973));
#39275=CARTESIAN_POINT('Ctrl Pts',(4.18745357006455,14.5517942140162,-4.44089209850063E-16));
#39276=CARTESIAN_POINT('Ctrl Pts',(4.18745357006455,14.5517942140162,-0.13066680730557));
#39277=CARTESIAN_POINT('Ctrl Pts',(4.18100368362964,14.5536548201376,-0.261069786498731));
#39278=CARTESIAN_POINT('Ctrl Pts',(4.16817103415993,14.5573291670729,-0.390710450871123));
#39279=CARTESIAN_POINT('Ctrl Pts',(4.15518429935153,14.561047632956,-0.521907748246283));
#39280=CARTESIAN_POINT('Ctrl Pts',(4.13566054561854,14.5666236366129,-0.652324314224272));
#39281=CARTESIAN_POINT('Ctrl Pts',(4.10965488440249,14.5739568744946,-0.781443489202978));
#39282=CARTESIAN_POINT('Ctrl Pts',(4.08920880779353,14.5797223861759,-0.882959098491578));
#39283=CARTESIAN_POINT('Ctrl Pts',(4.06475571708163,14.586573067282,-0.983672743459539));
#39284=CARTESIAN_POINT('Ctrl Pts',(4.0363167267713,14.5944383081264,-1.08333333333333));
#39285=CARTESIAN_POINT('',(3.972545991042,13.685078675306,-1.08333333333333));
#39286=CARTESIAN_POINT('Ctrl Pts',(4.0363167267713,14.5944383081264,-1.08333333333333));
#39287=CARTESIAN_POINT('Ctrl Pts',(4.06125577389196,14.4784021699801,-1.08333333333333));
#39288=CARTESIAN_POINT('Ctrl Pts',(4.07292947680577,14.3589061390379,-1.08333333333333));
#39289=CARTESIAN_POINT('Ctrl Pts',(4.07292947680577,14.0696859538867,-1.08333333333333));
#39290=CARTESIAN_POINT('Ctrl Pts',(4.03699073486612,13.8609255570161,-1.08333333333333));
#39291=CARTESIAN_POINT('Ctrl Pts',(3.97254599104201,13.685078675306,-1.08333333333333));
#39292=CARTESIAN_POINT('Ctrl Pts',(3.97254599103891,13.6850786752974,-1.08333333333318));
#39293=CARTESIAN_POINT('Ctrl Pts',(4.00550358468898,13.6755116454224,-0.949622058007565));
#39294=CARTESIAN_POINT('Ctrl Pts',(4.03223833992508,13.667626413385,-0.814376693553222));
#39295=CARTESIAN_POINT('Ctrl Pts',(4.05275116551691,13.6615412011384,-0.678132403728152));
#39296=CARTESIAN_POINT('Ctrl Pts',(4.07316650047532,13.6554849098804,-0.542535637670838));
#39297=CARTESIAN_POINT('Ctrl Pts',(4.0874189867075,13.6512115628239,-0.40594941879892));
#39298=CARTESIAN_POINT('Ctrl Pts',(4.09549564973878,13.6487880554638,-0.268901316711817));
#39299=CARTESIAN_POINT('Ctrl Pts',(4.10076932144717,13.6472056219574,-0.179415511018788));
#39300=CARTESIAN_POINT('Ctrl Pts',(4.10340966592831,13.6464108509735,-0.0897327832366672));
#39301=CARTESIAN_POINT('Ctrl Pts',(4.10340966592831,13.6464108509735,4.66293670342566E-15));
#39302=CARTESIAN_POINT('Ctrl Pts',(4.10340966592831,13.6464108509735,0.137573936980382));
#39303=CARTESIAN_POINT('Ctrl Pts',(4.09720533291532,13.6482810316174,0.274951212619736));
#39304=CARTESIAN_POINT('Ctrl Pts',(4.08483748845152,13.6519816397819,0.41161240621476));
#39305=CARTESIAN_POINT('Ctrl Pts',(4.07237395114171,13.6557108803995,0.549330978772818));
#39306=CARTESIAN_POINT('Ctrl Pts',(4.05365110225785,13.6612989721827,0.686322345436846));
#39307=CARTESIAN_POINT('Ctrl Pts',(4.02869583028489,13.6686542829587,0.822054935347102));
#39308=CARTESIAN_POINT('Ctrl Pts',(4.01257796374822,13.6734048590114,0.909720570537157));
#39309=CARTESIAN_POINT('Ctrl Pts',(3.99385994844905,13.6788915953345,0.996861109122728));
#39310=CARTESIAN_POINT('Ctrl Pts',(3.97254599103891,13.6850786752974,1.08333333333318));
#39311=CARTESIAN_POINT('Origin',(0.,0.,1.08333333333333));
#39312=CARTESIAN_POINT('Origin',(0.,0.,-1.08333333333333));
#39313=CARTESIAN_POINT('Origin',(0.,0.,1.08333333333333));
#39314=CARTESIAN_POINT('Origin',(0.,0.,1.08333333333333));
#39315=CARTESIAN_POINT('Origin',(0.,0.,1.08333333333333));
#39316=CARTESIAN_POINT('Origin',(0.,0.,-1.08333333333333));
#39317=CARTESIAN_POINT('Origin',(0.,0.,1.08333333333333));
#39318=CARTESIAN_POINT('Origin',(0.,0.,-1.08333333333333));
#39319=CARTESIAN_POINT('Origin',(0.,15.1423076923077,3.45272288248773));
#39320=CARTESIAN_POINT('Origin',(0.,13.3576923076923,3.45272288248773));
#39321=CARTESIAN_POINT('Origin',(0.,0.,1.08333333333333));
#39322=CARTESIAN_POINT('Origin',(0.,0.,1.08333333333333));
#39323=CARTESIAN_POINT('Origin',(0.,0.,1.08333333333333));
#39324=CARTESIAN_POINT('Origin',(0.,0.,-1.08333333333333));
#39325=CARTESIAN_POINT('Origin',(0.,0.,-1.08333333333333));
#39326=CARTESIAN_POINT('Origin',(0.,0.,-1.08333333333333));
#39327=CARTESIAN_POINT('Origin',(0.,0.,1.08333333333333));
#39328=CARTESIAN_POINT('Origin',(0.,0.,1.08333333333333));
#39329=CARTESIAN_POINT('Origin',(10.4434643792748,8.32838493021314,3.45272288248773));
#39330=CARTESIAN_POINT('Origin',(11.8387328710639,9.44107442276104,3.45272288248773));
#39331=CARTESIAN_POINT('Origin',(-1.55588456152528E-16,7.49274514625042E-17,
-1.08333333333333));
#39332=CARTESIAN_POINT('Origin',(-1.55588456152528E-16,7.49274514625042E-17,
-1.08333333333333));
#39333=CARTESIAN_POINT('Origin',(-1.55588456152528E-16,7.49274514625042E-17,
-1.08333333333333));
#39334=CARTESIAN_POINT('Origin',(1.55588456152528E-16,-7.49274514625042E-17,
1.08333333333333));
#39335=CARTESIAN_POINT('Origin',(1.55588456152528E-16,-7.49274514625042E-17,
1.08333333333333));
#39336=CARTESIAN_POINT('Origin',(1.55588456152528E-16,-7.49274514625042E-17,
1.08333333333333));
#39337=CARTESIAN_POINT('Origin',(1.55588456152528E-16,-7.49274514625042E-17,
1.08333333333333));
#39338=CARTESIAN_POINT('Origin',(1.55588456152528E-16,-7.49274514625042E-17,
1.08333333333333));
#39339=CARTESIAN_POINT('Origin',(1.94015631396094E-16,-2.43287906657286E-16,
1.08333333333333));
#39340=CARTESIAN_POINT('Origin',(1.94015631396094E-16,-2.43287906657286E-16,
1.08333333333333));
#39341=CARTESIAN_POINT('Origin',(-1.94015631396094E-16,2.43287906657286E-16,
-1.08333333333333));
#39342=CARTESIAN_POINT('Origin',(1.94015631396094E-16,-2.43287906657286E-16,
1.08333333333333));
#39343=CARTESIAN_POINT('Origin',(-1.94015631396094E-16,2.43287906657286E-16,
-1.08333333333333));
#39344=CARTESIAN_POINT('Origin',(1.94015631396094E-16,-2.43287906657286E-16,
1.08333333333333));
#39345=CARTESIAN_POINT('Origin',(-1.94015631396094E-16,2.43287906657286E-16,
-1.08333333333333));
#39346=CARTESIAN_POINT('Origin',(1.94015631396094E-16,-2.43287906657286E-16,
1.08333333333333));
#39347=CARTESIAN_POINT('Origin',(13.0227870731057,-2.97236616780865,3.45272288248773));
#39348=CARTESIAN_POINT('Origin',(14.7626584240763,-3.36948044994605,3.45272288248773));
#39349=CARTESIAN_POINT('Origin',(-1.94015631396094E-16,2.43287906657286E-16,
-1.08333333333333));
#39350=CARTESIAN_POINT('Origin',(-1.94015631396094E-16,2.43287906657286E-16,
-1.08333333333333));
#39351=CARTESIAN_POINT('Origin',(-1.94015631396094E-16,2.43287906657286E-16,
-1.08333333333333));
#39352=CARTESIAN_POINT('Origin',(1.94015631396094E-16,-2.43287906657286E-16,
1.08333333333333));
#39353=CARTESIAN_POINT('Origin',(1.94015631396094E-16,-2.43287906657286E-16,
1.08333333333333));
#39354=CARTESIAN_POINT('Origin',(1.94015631396094E-16,-2.43287906657286E-16,
1.08333333333333));
#39355=CARTESIAN_POINT('Origin',(1.94015631396094E-16,-2.43287906657286E-16,
1.08333333333333));
#39356=CARTESIAN_POINT('Origin',(1.94015631396094E-16,-2.43287906657286E-16,
1.08333333333333));
#39357=CARTESIAN_POINT('Origin',(8.63450790007668E-17,-3.78302508895262E-16,
1.08333333333333));
#39358=CARTESIAN_POINT('Origin',(8.63450790007668E-17,-3.78302508895262E-16,
1.08333333333333));
#39359=CARTESIAN_POINT('Origin',(-8.63450790007668E-17,3.78302508895262E-16,
-1.08333333333333));
#39360=CARTESIAN_POINT('Origin',(8.63450790007668E-17,-3.78302508895262E-16,
1.08333333333333));
#39361=CARTESIAN_POINT('Origin',(-8.63450790007668E-17,3.78302508895262E-16,
-1.08333333333333));
#39362=CARTESIAN_POINT('Origin',(8.63450790007668E-17,-3.78302508895262E-16,
1.08333333333333));
#39363=CARTESIAN_POINT('Origin',(-8.63450790007668E-17,3.78302508895262E-16,
-1.08333333333333));
#39364=CARTESIAN_POINT('Origin',(8.63450790007668E-17,-3.78302508895262E-16,
1.08333333333333));
#39365=CARTESIAN_POINT('Origin',(5.79568548444348,-12.0348649162504,3.45272288248773));
#39366=CARTESIAN_POINT('Origin',(6.57000108040713,-13.6427478189685,3.45272288248772));
#39367=CARTESIAN_POINT('Origin',(-8.63450790007668E-17,3.78302508895262E-16,
-1.08333333333333));
#39368=CARTESIAN_POINT('Origin',(-8.63450790007668E-17,3.78302508895262E-16,
-1.08333333333333));
#39369=CARTESIAN_POINT('Origin',(-8.63450790007668E-17,3.78302508895262E-16,
-1.08333333333333));
#39370=CARTESIAN_POINT('Origin',(8.63450790007668E-17,-3.78302508895262E-16,
1.08333333333333));
#39371=CARTESIAN_POINT('Origin',(8.63450790007668E-17,-3.78302508895262E-16,
1.08333333333333));
#39372=CARTESIAN_POINT('Origin',(8.63450790007668E-17,-3.78302508895262E-16,
1.08333333333333));
#39373=CARTESIAN_POINT('Origin',(8.63450790007668E-17,-3.78302508895262E-16,
1.08333333333333));
#39374=CARTESIAN_POINT('Origin',(8.63450790007668E-17,-3.78302508895262E-16,
1.08333333333333));
#39375=CARTESIAN_POINT('Origin',(-8.63450790007644E-17,-3.78302508895264E-16,
1.08333333333333));
#39376=CARTESIAN_POINT('Origin',(-8.63450790007644E-17,-3.78302508895264E-16,
1.08333333333333));
#39377=CARTESIAN_POINT('Origin',(8.63450790007644E-17,3.78302508895264E-16,
-1.08333333333333));
#39378=CARTESIAN_POINT('Origin',(-8.63450790007644E-17,-3.78302508895264E-16,
1.08333333333333));
#39379=CARTESIAN_POINT('Origin',(8.63450790007644E-17,3.78302508895264E-16,
-1.08333333333333));
#39380=CARTESIAN_POINT('Origin',(-8.63450790007644E-17,-3.78302508895264E-16,
1.08333333333333));
#39381=CARTESIAN_POINT('Origin',(8.63450790007644E-17,3.78302508895264E-16,
-1.08333333333333));
#39382=CARTESIAN_POINT('Origin',(-8.63450790007644E-17,-3.78302508895264E-16,
1.08333333333333));
#39383=CARTESIAN_POINT('Origin',(-5.79568548444331,-12.0348649162504,3.45272288248773));
#39384=CARTESIAN_POINT('Origin',(-6.57000108040694,-13.6427478189686,3.45272288248772));
#39385=CARTESIAN_POINT('Origin',(8.63450790007644E-17,3.78302508895264E-16,
-1.08333333333333));
#39386=CARTESIAN_POINT('Origin',(8.63450790007644E-17,3.78302508895264E-16,
-1.08333333333333));
#39387=CARTESIAN_POINT('Origin',(8.63450790007644E-17,3.78302508895264E-16,
-1.08333333333333));
#39388=CARTESIAN_POINT('Origin',(-8.63450790007644E-17,-3.78302508895264E-16,
1.08333333333333));
#39389=CARTESIAN_POINT('Origin',(-8.63450790007644E-17,-3.78302508895264E-16,
1.08333333333333));
#39390=CARTESIAN_POINT('Origin',(-8.63450790007644E-17,-3.78302508895264E-16,
1.08333333333333));
#39391=CARTESIAN_POINT('Origin',(-8.63450790007644E-17,-3.78302508895264E-16,
1.08333333333333));
#39392=CARTESIAN_POINT('Origin',(-8.63450790007644E-17,-3.78302508895264E-16,
1.08333333333333));
#39393=CARTESIAN_POINT('Origin',(-1.94015631396093E-16,-2.43287906657289E-16,
1.08333333333333));
#39394=CARTESIAN_POINT('Origin',(-1.94015631396093E-16,-2.43287906657289E-16,
1.08333333333333));
#39395=CARTESIAN_POINT('Origin',(1.94015631396093E-16,2.43287906657289E-16,
-1.08333333333333));
#39396=CARTESIAN_POINT('Origin',(-1.94015631396093E-16,-2.43287906657289E-16,
1.08333333333333));
#39397=CARTESIAN_POINT('Origin',(1.94015631396093E-16,2.43287906657289E-16,
-1.08333333333333));
#39398=CARTESIAN_POINT('Origin',(-1.94015631396093E-16,-2.43287906657289E-16,
1.08333333333333));
#39399=CARTESIAN_POINT('Origin',(1.94015631396093E-16,2.43287906657289E-16,
-1.08333333333333));
#39400=CARTESIAN_POINT('Origin',(-1.94015631396093E-16,-2.43287906657289E-16,
1.08333333333333));
#39401=CARTESIAN_POINT('Origin',(-13.0227870731057,-2.97236616780882,3.45272288248773));
#39402=CARTESIAN_POINT('Origin',(-14.7626584240763,-3.36948044994625,3.45272288248773));
#39403=CARTESIAN_POINT('Origin',(1.94015631396093E-16,2.43287906657289E-16,
-1.08333333333333));
#39404=CARTESIAN_POINT('Origin',(1.94015631396093E-16,2.43287906657289E-16,
-1.08333333333333));
#39405=CARTESIAN_POINT('Origin',(1.94015631396093E-16,2.43287906657289E-16,
-1.08333333333333));
#39406=CARTESIAN_POINT('Origin',(-1.94015631396093E-16,-2.43287906657289E-16,
1.08333333333333));
#39407=CARTESIAN_POINT('Origin',(-1.94015631396093E-16,-2.43287906657289E-16,
1.08333333333333));
#39408=CARTESIAN_POINT('Origin',(-1.94015631396093E-16,-2.43287906657289E-16,
1.08333333333333));
#39409=CARTESIAN_POINT('Origin',(-1.94015631396093E-16,-2.43287906657289E-16,
1.08333333333333));
#39410=CARTESIAN_POINT('Origin',(-1.94015631396093E-16,-2.43287906657289E-16,
1.08333333333333));
#39411=CARTESIAN_POINT('Origin',(-1.55588456152529E-16,-7.49274514625064E-17,
1.08333333333333));
#39412=CARTESIAN_POINT('Origin',(-1.55588456152529E-16,-7.49274514625064E-17,
1.08333333333333));
#39413=CARTESIAN_POINT('Origin',(1.55588456152529E-16,7.49274514625064E-17,
-1.08333333333333));
#39414=CARTESIAN_POINT('Origin',(-1.55588456152529E-16,-7.49274514625064E-17,
1.08333333333333));
#39415=CARTESIAN_POINT('Origin',(1.55588456152529E-16,7.49274514625064E-17,
-1.08333333333333));
#39416=CARTESIAN_POINT('Origin',(-1.55588456152529E-16,-7.49274514625064E-17,
1.08333333333333));
#39417=CARTESIAN_POINT('Origin',(1.55588456152529E-16,7.49274514625064E-17,
-1.08333333333333));
#39418=CARTESIAN_POINT('Origin',(-1.55588456152529E-16,-7.49274514625064E-17,
1.08333333333333));
#39419=CARTESIAN_POINT('Origin',(-10.4434643792749,8.32838493021299,3.45272288248773));
#39420=CARTESIAN_POINT('Origin',(-11.838732871064,9.44107442276088,3.45272288248773));
#39421=CARTESIAN_POINT('Origin',(1.55588456152529E-16,7.49274514625064E-17,
-1.08333333333333));
#39422=CARTESIAN_POINT('Origin',(1.55588456152529E-16,7.49274514625064E-17,
-1.08333333333333));
#39423=CARTESIAN_POINT('Origin',(1.55588456152529E-16,7.49274514625064E-17,
-1.08333333333333));
#39424=CARTESIAN_POINT('Origin',(-1.55588456152529E-16,-7.49274514625064E-17,
1.08333333333333));
#39425=CARTESIAN_POINT('Origin',(-1.55588456152529E-16,-7.49274514625064E-17,
1.08333333333333));
#39426=CARTESIAN_POINT('Origin',(-1.55588456152529E-16,-7.49274514625064E-17,
1.08333333333333));
#39427=CARTESIAN_POINT('Origin',(-1.55588456152529E-16,-7.49274514625064E-17,
1.08333333333333));
#39428=CARTESIAN_POINT('Origin',(-1.55588456152529E-16,-7.49274514625064E-17,
1.08333333333333));
#39429=CARTESIAN_POINT('Origin',(0.,0.,1.08333333333333));
#39430=CARTESIAN_POINT('Origin',(0.,0.,1.08333333333333));
#39431=CARTESIAN_POINT('Origin',(0.,0.,1.08333333333333));
#39432=CARTESIAN_POINT('Origin',(0.,0.,-1.08333333333333));
#39433=CARTESIAN_POINT('Origin',(0.,0.,-1.08333333333333));
#39434=CARTESIAN_POINT('Origin',(0.,0.,-1.08333333333333));
#39435=CARTESIAN_POINT('Origin',(0.,0.,1.08333333333333));
#39436=CARTESIAN_POINT('Origin',(0.,0.,1.08333333333333));
#43765=UNCERTAINTY_MEASURE_WITH_UNIT(LENGTH_MEASURE(0.01),#43782,
'DISTANCE_ACCURACY_VALUE',
'Maximum model space distance between geometric entities at asserted c
onnectivities');
#43771=UNCERTAINTY_MEASURE_WITH_UNIT(LENGTH_MEASURE(0.01),#43782,
'DISTANCE_ACCURACY_VALUE',
'Maximum model space distance between geometric entities at asserted c
onnectivities');
#43775=(
GEOMETRIC_REPRESENTATION_CONTEXT(3)
GLOBAL_UNCERTAINTY_ASSIGNED_CONTEXT((#43765))
GLOBAL_UNIT_ASSIGNED_CONTEXT((#43782,#43784,#43785))
REPRESENTATION_CONTEXT('','3D')
);
#43781=(
GEOMETRIC_REPRESENTATION_CONTEXT(3)
GLOBAL_UNCERTAINTY_ASSIGNED_CONTEXT((#43771))
GLOBAL_UNIT_ASSIGNED_CONTEXT((#43782,#43784,#43785))
REPRESENTATION_CONTEXT('','3D')
);
#43782=(
LENGTH_UNIT()
NAMED_UNIT(*)
SI_UNIT(.MILLI.,.METRE.)
);
#43784=(
NAMED_UNIT(*)
PLANE_ANGLE_UNIT()
SI_UNIT($,.RADIAN.)
);
#43785=(
NAMED_UNIT(*)
SI_UNIT($,.STERADIAN.)
SOLID_ANGLE_UNIT()
);
#43789=SHAPE_DEFINITION_REPRESENTATION(#43798,#43815);
#43798=PRODUCT_DEFINITION_SHAPE('',$,#43825);
#43815=SHAPE_REPRESENTATION('',(#13627),#43775);
#43821=PRODUCT_DEFINITION_CONTEXT('part definition',#43850,'design');
#43825=PRODUCT_DEFINITION('5972K117_Steel Ball Bearing','Bearing_01',#43834,
#43821);
#43834=PRODUCT_DEFINITION_FORMATION('',$,#43855);
#43850=APPLICATION_CONTEXT(
'Core Data for Automotive Mechanical Design Process');
#43851=PRODUCT_CONTEXT('part definition',#43850,'mechanical');
#43855=PRODUCT('5972K117_Steel Ball Bearing','Bearing_01',$,(#43851));
#43863=PRESENTATION_STYLE_ASSIGNMENT((#43866));
#43866=SURFACE_STYLE_USAGE(.BOTH.,#43869);
#43869=SURFACE_SIDE_STYLE('',(#43872));
#43872=SURFACE_STYLE_FILL_AREA(#43875);
#43875=FILL_AREA_STYLE('Opaque(160,160,160)',(#43878));
#43878=FILL_AREA_STYLE_COLOUR('Opaque(160,160,160)',#43881);
#43881=COLOUR_RGB('Opaque(160,160,160)', 0.31764706, 0.68627451, 0.89019608);
ENDSEC;
END-ISO-10303-21;
